ISO-10303-21;
HEADER;
FILE_DESCRIPTION (('STEP AP214'),
    '1' );
FILE_NAME ('radial cylindrical roller bearing_iso_ISO 15 RCR - 17200 - 54,SI,NC,54.step',
    '2026-09-30T13:58:28',
    ( '' ),
    ( '' ),
    'SwSTEP 2.0',
    'SolidWorks 2026',
    '' );
FILE_SCHEMA (( 'AUTOMOTIVE_DESIGN' ));
ENDSEC;

DATA;
#91=CIRCLE ( 'NONE', #1856, 113.8250000000000171 ) ;
#140=CARTESIAN_POINT ( 'NONE',  ( -90.00000000000000000, 0.000000000000000000, 0.000000000000000000 ) ) ;
#153=CIRCLE ( 'NONE', #7560, 120.0000000000000568 ) ;
#154=FILL_AREA_STYLE ('',( #18612 ) ) ;
#212=CARTESIAN_POINT ( 'NONE',  ( 10.00000000000000888, 0.000000000000000000, 0.000000000000000000 ) ) ;
#302=CARTESIAN_POINT ( 'NONE',  ( -10.00000000000000888, 0.000000000000000000, 0.000000000000000000 ) ) ;
#328=AXIS2_PLACEMENT_3D ( 'NONE', #9035, #9242, #14226 ) ;
#340=DIRECTION ( 'NONE',  ( 0.000000000000000000, 1.224646799147354933E-16, 1.000000000000000000 ) ) ;
#345=DIRECTION ( 'NONE',  ( 0.000000000000000000, 0.000000000000000000, -1.000000000000000000 ) ) ;
#388=LINE ( 'NONE', #20601, #18757 ) ;
#411=CIRCLE ( 'NONE', #3579, 113.8250000000000171 ) ;
#434=CARTESIAN_POINT ( 'NONE',  ( 8.899999999999989697, 1.238117913937974620E-14, 101.1000000000000512 ) ) ;
#445=EDGE_CURVE ( 'NONE', #19369, #15511, #13481, .T. ) ;
#458=ORIENTED_EDGE ( 'NONE', *, *, #7475, .F. ) ;
#485=CIRCLE ( 'NONE', #20594, 104.9000000000000341 ) ;
#486=AXIS2_PLACEMENT_3D ( 'NONE', #4785, #9859, #11408 ) ;
#490=CARTESIAN_POINT ( 'NONE',  ( -90.00000000000000000, 0.000000000000000000, 0.000000000000000000 ) ) ;
#492=CARTESIAN_POINT ( 'NONE',  ( 9.999999999999994671, 0.000000000000000000, 0.000000000000000000 ) ) ;
#496=CARTESIAN_POINT ( 'NONE',  ( -90.00000000000000000, 0.000000000000000000, -115.1000000000000227 ) ) ;
#512=CARTESIAN_POINT ( 'NONE',  ( -8.000000000000007105, 1.284654492305574008E-14, 104.9000000000000341 ) ) ;
#556=ORIENTED_EDGE ( 'NONE', *, *, #17340, .T. ) ;
#599=DIRECTION ( 'NONE',  ( 1.000000000000000000, 0.000000000000000000, 0.000000000000000000 ) ) ;
#624=DIRECTION ( 'NONE',  ( -0.000000000000000000, 0.000000000000000000, 1.000000000000000000 ) ) ;
#626=CARTESIAN_POINT ( 'NONE',  ( 7.440711023145602176, 0.000000000000000000, 0.000000000000000000 ) ) ;
#661=AXIS2_PLACEMENT_3D ( 'NONE', #13901, #18996, #17342 ) ;
#669=ORIENTED_EDGE ( 'NONE', *, *, #11797, .T. ) ;
#694=ADVANCED_FACE ( 'NONE', ( #3962 ), #7170, .T. ) ;
#699=AXIS2_PLACEMENT_3D ( 'NONE', #2722, #7806, #14768 ) ;
#708=DIRECTION ( 'NONE',  ( 0.000000000000000000, 0.000000000000000000, -1.000000000000000000 ) ) ;
#726=ORIENTED_EDGE ( 'NONE', *, *, #7475, .T. ) ;
#735=DIRECTION ( 'NONE',  ( 1.000000000000000000, -0.000000000000000000, -0.000000000000000000 ) ) ;
#753=CYLINDRICAL_SURFACE ( 'NONE', #328, 120.0000000000000426 ) ;
#760=CARTESIAN_POINT ( 'NONE',  ( -10.00000000000000888, 0.000000000000000000, 0.000000000000000000 ) ) ;
#767=ORIENTED_EDGE ( 'NONE', *, *, #6366, .T. ) ;
#802=CARTESIAN_POINT ( 'NONE',  ( -10.00000000000002309, 0.000000000000000000, -118.9000000000000199 ) ) ;
#840=AXIS2_PLACEMENT_3D ( 'NONE', #16403, #19825, #9765 ) ;
#856=EDGE_CURVE ( 'NONE', #18401, #7456, #8589, .T. ) ;
#867=AXIS2_PLACEMENT_3D ( 'NONE', #14370, #5988, #12707 ) ;
#869=DIRECTION ( 'NONE',  ( 0.000000000000000000, 1.224646799147322392E-16, 1.000000000000000000 ) ) ;
#884=CARTESIAN_POINT ( 'NONE',  ( -7.600000000000001421, 0.000000000000000000, -105.0992000000000104 ) ) ;
#889=CARTESIAN_POINT ( 'NONE',  ( 7.395800000000001262, 0.000000000000000000, 0.000000000000000000 ) ) ;
#921=DIRECTION ( 'NONE',  ( 1.000000000000000000, 0.000000000000000000, 0.000000000000000000 ) ) ;
#937=EDGE_CURVE ( 'NONE', #11505, #5209, #18071, .T. ) ;
#967=EDGE_LOOP ( 'NONE', ( #4820, #9841, #7044, #8033 ) ) ;
#985=ADVANCED_FACE ( 'NONE', ( #2272 ), #16987, .T. ) ;
#993=VERTEX_POINT ( 'NONE', #7052 ) ;
#1001=ADVANCED_FACE ( 'NONE', ( #3935, #15432 ), #15758, .T. ) ;
#1005=DIRECTION ( 'NONE',  ( 0.000000000000000000, 0.000000000000000000, 1.000000000000000000 ) ) ;
#1045=AXIS2_PLACEMENT_3D ( 'NONE', #3352, #1383, #4916 ) ;
#1093=EDGE_CURVE ( 'NONE', #3248, #19526, #4523, .T. ) ;
#1114=CARTESIAN_POINT ( 'NONE',  ( 7.599999999999998757, 0.000000000000000000, -105.0992000000000104 ) ) ;
#1142=ADVANCED_FACE ( 'NONE', ( #14644, #12759 ), #12545, .T. ) ;
#1171=ORIENTED_EDGE ( 'NONE', *, *, #9708, .F. ) ;
#1245=VERTEX_POINT ( 'NONE', #10102 ) ;
#1268=DIRECTION ( 'NONE',  ( 0.000000000000000000, 0.000000000000000000, -1.000000000000000000 ) ) ;
#1273=ORIENTED_EDGE ( 'NONE', *, *, #3235, .T. ) ;
#1280=FACE_OUTER_BOUND ( 'NONE', #14242, .T. ) ;
#1289=UNCERTAINTY_MEASURE_WITH_UNIT (LENGTH_MEASURE( 1.000000000000000082E-05 ), #15116, 'distance_accuracy_value', 'NONE');
#1292=CIRCLE ( 'NONE', #13628, 105.0992000000000104 ) ;
#1314=FACE_OUTER_BOUND ( 'NONE', #13417, .T. ) ;
#1361=DIRECTION ( 'NONE',  ( 0.000000000000000000, 0.000000000000000000, -1.000000000000000000 ) ) ;
#1383=DIRECTION ( 'NONE',  ( 1.000000000000000000, 0.000000000000000000, 0.000000000000000000 ) ) ;
#1406=PLANE ( 'NONE',  #3872 ) ;
#1419=CIRCLE ( 'NONE', #699, 115.1000000000000227 ) ;
#1436=ORIENTED_EDGE ( 'NONE', *, *, #13673, .F. ) ;
#1457=ORIENTED_EDGE ( 'NONE', *, *, #9041, .F. ) ;
#1481=EDGE_LOOP ( 'NONE', ( #15119, #8761, #15682, #11730 ) ) ;
#1529=VERTEX_POINT ( 'NONE', #802 ) ;
#1539=EDGE_CURVE ( 'NONE', #21817, #5871, #12841, .T. ) ;
#1540=EDGE_LOOP ( 'NONE', ( #6165, #4258 ) ) ;
#1546=AXIS2_PLACEMENT_3D ( 'NONE', #7056, #20313, #8701 ) ;
#1583=TOROIDAL_SURFACE ( 'NONE', #20640, 114.9007999999999896, 0.2042000000000016025 ) ;
#1605=LINE ( 'NONE', #15075, #10024 ) ;
#1609=VERTEX_POINT ( 'NONE', #14398 ) ;
#1633=CARTESIAN_POINT ( 'NONE',  ( -8.900000000000019895, 0.000000000000000000, 0.000000000000000000 ) ) ;
#1647=FILL_AREA_STYLE ('',( #16781 ) ) ;
#1651=PLANE ( 'NONE',  #14411 ) ;
#1656=VERTEX_POINT ( 'NONE', #21151 ) ;
#1667=CIRCLE ( 'NONE', #14007, 104.9000000000000341 ) ;
#1671=ORIENTED_EDGE ( 'NONE', *, *, #2549, .T. ) ;
#1688=PLANE ( 'NONE',  #20653 ) ;
#1762=ADVANCED_FACE ( 'NONE', ( #11734 ), #12122, .T. ) ;
#1763=ORIENTED_EDGE ( 'NONE', *, *, #2386, .F. ) ;
#1765=DIRECTION ( 'NONE',  ( 1.000000000000000000, 0.000000000000000000, 0.000000000000000000 ) ) ;
#1772=CARTESIAN_POINT ( 'NONE',  ( -90.00000000000000000, 0.000000000000000000, 0.000000000000000000 ) ) ;
#1796=EDGE_CURVE ( 'NONE', #2646, #8089, #18835, .T. ) ;
#1811=SURFACE_STYLE_USAGE ( .BOTH. , #15387 ) ;
#1812=ORIENTED_EDGE ( 'NONE', *, *, #1539, .T. ) ;
#1841=VERTEX_POINT ( 'NONE', #7205 ) ;
#1856=AXIS2_PLACEMENT_3D ( 'NONE', #9918, #8058, #10136 ) ;
#1862=AXIS2_PLACEMENT_3D ( 'NONE', #6857, #11711, #6647 ) ;
#1887=EDGE_CURVE ( 'NONE', #5459, #12003, #5582, .T. ) ;
#1909=DIRECTION ( 'NONE',  ( 0.000000000000000000, 0.000000000000000000, -1.000000000000000000 ) ) ;
#1919=EDGE_LOOP ( 'NONE', ( #8029, #15366 ) ) ;
#1933=EDGE_CURVE ( 'NONE', #9325, #12372, #20755, .T. ) ;
#1939=EDGE_CURVE ( 'NONE', #1529, #21817, #15815, .T. ) ;
#1942=AXIS2_PLACEMENT_3D ( 'NONE', #760, #2523, #14236 ) ;
#1944=TOROIDAL_SURFACE ( 'NONE', #4051, 114.9007999999999896, 0.2042000000000016025 ) ;
#1948=CIRCLE ( 'NONE', #10754, 114.9007999999999896 ) ;
#1981=EDGE_LOOP ( 'NONE', ( #7969, #21412, #17685, #15866 ) ) ;
#1991=DIRECTION ( 'NONE',  ( -1.000000000000000000, 0.000000000000000000, 0.000000000000000000 ) ) ;
#2009=CIRCLE ( 'NONE', #3083, 113.8250000000000028 ) ;
#2019=VERTEX_POINT ( 'NONE', #10726 ) ;
#2020=CIRCLE ( 'NONE', #3782, 0.2042000000000016025 ) ;
#2036=FACE_OUTER_BOUND ( 'NONE', #11625, .T. ) ;
#2054=AXIS2_PLACEMENT_3D ( 'NONE', #11605, #1765, #19882 ) ;
#2101=PRODUCT_DEFINITION_CONTEXT ( 'detailed design', #2331, 'design' ) ;
#2111=LINE ( 'NONE', #8842, #8332 ) ;
#2128=CARTESIAN_POINT ( 'NONE',  ( 8.899999999999987921, 0.000000000000000000, -118.9000000000000199 ) ) ;
#2169=DIRECTION ( 'NONE',  ( 0.000000000000000000, 0.000000000000000000, -1.000000000000000000 ) ) ;
#2252=ORIENTED_EDGE ( 'NONE', *, *, #16247, .T. ) ;
#2272=FACE_OUTER_BOUND ( 'NONE', #4924, .T. ) ;
#2276=DIRECTION ( 'NONE',  ( 0.000000000000000000, 0.000000000000000000, -1.000000000000000000 ) ) ;
#2280=CARTESIAN_POINT ( 'NONE',  ( -8.900000000000018119, 0.000000000000000000, 0.000000000000000000 ) ) ;
#2284=ADVANCED_FACE ( 'NONE', ( #8704 ), #17538, .F. ) ;
#2291=ORIENTED_EDGE ( 'NONE', *, *, #6500, .F. ) ;
#2320=ORIENTED_EDGE ( 'NONE', *, *, #3783, .F. ) ;
#2331=APPLICATION_CONTEXT ( 'automotive_design' ) ;
#2334=CARTESIAN_POINT ( 'NONE',  ( -10.00000000000001243, 0.000000000000000000, -101.1000000000000369 ) ) ;
#2342=CARTESIAN_POINT ( 'NONE',  ( -90.00000000000000000, 0.000000000000000000, 0.000000000000000000 ) ) ;
#2343=EDGE_CURVE ( 'NONE', #5948, #1656, #20876, .T. ) ;
#2344=LINE ( 'NONE', #11062, #17237 ) ;
#2360=DIRECTION ( 'NONE',  ( 1.000000000000000000, 0.000000000000000000, 0.000000000000000000 ) ) ;
#2366=VECTOR ( 'NONE', #15346, 1000.000000000000000 ) ;
#2386=EDGE_CURVE ( 'NONE', #1656, #6035, #19625, .T. ) ;
#2428=AXIS2_PLACEMENT_3D ( 'NONE', #2128, #8858, #13940 ) ;
#2445=DIRECTION ( 'NONE',  ( 0.000000000000000000, 0.000000000000000000, -1.000000000000000000 ) ) ;
#2485=EDGE_CURVE ( 'NONE', #8212, #993, #8388, .T. ) ;
#2486=DIRECTION ( 'NONE',  ( 1.000000000000000000, 0.000000000000000000, 0.000000000000000000 ) ) ;
#2499=LINE ( 'NONE', #7802, #7891 ) ;
#2517=DIRECTION ( 'NONE',  ( 0.000000000000000000, 0.000000000000000000, -1.000000000000000000 ) ) ;
#2523=DIRECTION ( 'NONE',  ( 1.000000000000000000, 0.000000000000000000, 0.000000000000000000 ) ) ;
#2538=CARTESIAN_POINT ( 'NONE',  ( -7.600000000000002309, 0.000000000000000000, 0.000000000000000000 ) ) ;
#2549=EDGE_CURVE ( 'NONE', #21817, #20730, #19790, .T. ) ;
#2565=CARTESIAN_POINT ( 'NONE',  ( 7.599999999999998757, 0.000000000000000000, -114.9007999999999896 ) ) ;
#2586=CARTESIAN_POINT ( 'NONE',  ( -90.00000000000000000, 1.284654492305574008E-14, 104.9000000000000341 ) ) ;
#2589=( LENGTH_UNIT ( ) NAMED_UNIT ( * ) SI_UNIT ( .MILLI., .METRE. ) );
#2591=ORIENTED_EDGE ( 'NONE', *, *, #13060, .F. ) ;
#2599=CARTESIAN_POINT ( 'NONE',  ( -7.395800000000001262, 0.000000000000000000, 0.000000000000000000 ) ) ;
#2600=CARTESIAN_POINT ( 'NONE',  ( -7.599999999999999645, 114.9007999999999896, 0.000000000000000000 ) ) ;
#2601=CARTESIAN_POINT ( 'NONE',  ( 7.999999999999979572, 0.000000000000000000, -115.1000000000000227 ) ) ;
#2603=DIRECTION ( 'NONE',  ( 0.000000000000000000, 0.000000000000000000, 1.000000000000000000 ) ) ;
#2616=DIRECTION ( 'NONE',  ( 1.000000000000000000, 0.000000000000000000, 0.000000000000000000 ) ) ;
#2621=ORIENTED_EDGE ( 'NONE', *, *, #17837, .T. ) ;
#2638=TOROIDAL_SURFACE ( 'NONE', #15701, 118.9000000000000199, 1.100000000000015854 ) ;
#2646=VERTEX_POINT ( 'NONE', #8349 ) ;
#2659=CARTESIAN_POINT ( 'NONE',  ( -8.000000000000007105, 0.000000000000000000, 0.000000000000000000 ) ) ;
#2700=CARTESIAN_POINT ( 'NONE',  ( -90.00000000000000000, 0.000000000000000000, 0.000000000000000000 ) ) ;
#2710=EDGE_CURVE ( 'NONE', #12003, #5459, #14415, .T. ) ;
#2722=CARTESIAN_POINT ( 'NONE',  ( -7.440711023145607506, 0.000000000000000000, 0.000000000000000000 ) ) ;
#2735=DIRECTION ( 'NONE',  ( 1.000000000000000000, 0.000000000000000000, 0.000000000000000000 ) ) ;
#2761=EDGE_CURVE ( 'NONE', #12158, #11505, #388, .T. ) ;
#2769=VERTEX_POINT ( 'NONE', #12204 ) ;
#2788=EDGE_CURVE ( 'NONE', #12003, #3216, #20524, .T. ) ;
#2795=SHAPE_DEFINITION_REPRESENTATION ( #4917, #16445 ) ;
#2825=EDGE_CURVE ( 'NONE', #12372, #9325, #411, .T. ) ;
#2832=DIRECTION ( 'NONE',  ( 1.000000000000000000, 0.000000000000000000, 0.000000000000000000 ) ) ;
#2881=MECHANICAL_DESIGN_GEOMETRIC_PRESENTATION_REPRESENTATION('',(#21577),#20179);
#2889=DIRECTION ( 'NONE',  ( -1.000000000000000000, 0.000000000000000000, -0.000000000000000000 ) ) ;
#2932=DIRECTION ( 'NONE',  ( -0.000000000000000000, -1.000000000000000000, -0.000000000000000000 ) ) ;
#2938=LINE ( 'NONE', #18420, #13229 ) ;
#2941=AXIS2_PLACEMENT_3D ( 'NONE', #7872, #19583, #13058 ) ;
#3029=DIRECTION ( 'NONE',  ( 1.000000000000000000, 0.000000000000000000, 0.000000000000000000 ) ) ;
#3041=CARTESIAN_POINT ( 'NONE',  ( -8.900000000000018119, 0.000000000000000000, 0.000000000000000000 ) ) ;
#3083=AXIS2_PLACEMENT_3D ( 'NONE', #10700, #7402, #4729 ) ;
#3090=ORIENTED_EDGE ( 'NONE', *, *, #18408, .F. ) ;
#3146=ADVANCED_FACE ( 'NONE', ( #12173 ), #20253, .F. ) ;
#3151=EDGE_LOOP ( 'NONE', ( #2291, #12878, #13374, #13037 ) ) ;
#3215=DIRECTION ( 'NONE',  ( 0.000000000000000000, 1.224646799147353207E-16, 1.000000000000000000 ) ) ;
#3216=VERTEX_POINT ( 'NONE', #5338 ) ;
#3221=CYLINDRICAL_SURFACE ( 'NONE', #7679, 113.8250000000000171 ) ;
#3225=FACE_BOUND ( 'NONE', #21726, .T. ) ;
#3233=ADVANCED_FACE ( 'NONE', ( #12065 ), #17158, .F. ) ;
#3235=EDGE_CURVE ( 'NONE', #5871, #1245, #3866, .T. ) ;
#3245=EDGE_CURVE ( 'NONE', #7456, #18401, #20883, .T. ) ;
#3248=VERTEX_POINT ( 'NONE', #1114 ) ;
#3266=CIRCLE ( 'NONE', #8901, 105.0992000000000104 ) ;
#3270=ORIENTED_EDGE ( 'NONE', *, *, #16507, .F. ) ;
#3288=CARTESIAN_POINT ( 'NONE',  ( -8.000000000000007105, 0.000000000000000000, 0.000000000000000000 ) ) ;
#3306=CIRCLE ( 'NONE', #18119, 1.100000000000003642 ) ;
#3316=CYLINDRICAL_SURFACE ( 'NONE', #21768, 115.1000000000000227 ) ;
#3321=TOROIDAL_SURFACE ( 'NONE', #9296, 114.9007999999999896, 0.2041999999999998816 ) ;
#3331=AXIS2_PLACEMENT_3D ( 'NONE', #2599, #5706, #15966 ) ;
#3351=VERTEX_POINT ( 'NONE', #9070 ) ;
#3352=CARTESIAN_POINT ( 'NONE',  ( 9.999999999999994671, 118.9000000000000199, 0.000000000000000000 ) ) ;
#3355=DIRECTION ( 'NONE',  ( 0.000000000000000000, 0.000000000000000000, -1.000000000000000000 ) ) ;
#3402=DIRECTION ( 'NONE',  ( 1.000000000000000000, 0.000000000000000000, 0.000000000000000000 ) ) ;
#3411=EDGE_CURVE ( 'NONE', #6130, #3216, #7852, .T. ) ;
#3419=ORIENTED_EDGE ( 'NONE', *, *, #12687, .T. ) ;
#3426=CARTESIAN_POINT ( 'NONE',  ( -10.00000000000002309, 1.393954219129474843E-14, 113.8250000000000028 ) ) ;
#3450=CARTESIAN_POINT ( 'NONE',  ( -90.00000000000000000, 0.000000000000000000, 0.000000000000000000 ) ) ;
#3453=CARTESIAN_POINT ( 'NONE',  ( 9.999999999999994671, 101.1000000000000512, 0.000000000000000000 ) ) ;
#3509=DIRECTION ( 'NONE',  ( -1.000000000000000000, 0.000000000000000000, -0.000000000000000000 ) ) ;
#3537=EDGE_CURVE ( 'NONE', #5209, #11505, #20372, .T. ) ;
#3568=DIRECTION ( 'NONE',  ( 0.000000000000000000, 0.000000000000000000, -1.000000000000000000 ) ) ;
#3579=AXIS2_PLACEMENT_3D ( 'NONE', #13970, #921, #17513 ) ;
#3585=CYLINDRICAL_SURFACE ( 'NONE', #13569, 113.8250000000000171 ) ;
#3612=CARTESIAN_POINT ( 'NONE',  ( -8.900000000000019895, 1.231382356542664155E-14, 100.0000000000000284 ) ) ;
#3632=DIRECTION ( 'NONE',  ( 1.000000000000000000, 0.000000000000000000, 0.000000000000000000 ) ) ;
#3650=EDGE_CURVE ( 'NONE', #8089, #2646, #10827, .T. ) ;
#3715=ORIENTED_EDGE ( 'NONE', *, *, #13855, .F. ) ;
#3739=ORIENTED_EDGE ( 'NONE', *, *, #21717, .T. ) ;
#3776=DIRECTION ( 'NONE',  ( 0.000000000000000000, 0.000000000000000000, -1.000000000000000000 ) ) ;
#3782=AXIS2_PLACEMENT_3D ( 'NONE', #17457, #19214, #869 ) ;
#3783=EDGE_CURVE ( 'NONE', #19526, #15663, #2020, .T. ) ;
#3810=DIRECTION ( 'NONE',  ( 0.000000000000000000, -1.000000000000000000, 0.000000000000000000 ) ) ;
#3824=ORIENTED_EDGE ( 'NONE', *, *, #21343, .T. ) ;
#3826=ORIENTED_EDGE ( 'NONE', *, *, #4604, .T. ) ;
#3857=EDGE_LOOP ( 'NONE', ( #5946, #14474 ) ) ;
#3859=DIRECTION ( 'NONE',  ( 0.000000000000000000, 0.000000000000000000, -1.000000000000000000 ) ) ;
#3866=CIRCLE ( 'NONE', #2428, 1.100000000000017630 ) ;
#3872=AXIS2_PLACEMENT_3D ( 'NONE', #19837, #18197, #9662 ) ;
#3917=ORIENTED_EDGE ( 'NONE', *, *, #11441, .T. ) ;
#3924=CARTESIAN_POINT ( 'NONE',  ( -8.900000000000019895, 1.469576158976824302E-14, 120.0000000000000284 ) ) ;
#3931=ORIENTED_EDGE ( 'NONE', *, *, #10549, .T. ) ;
#3935=FACE_BOUND ( 'NONE', #13386, .T. ) ;
#3939=CARTESIAN_POINT ( 'NONE',  ( -10.00000000000002309, 0.000000000000000000, 0.000000000000000000 ) ) ;
#3962=FACE_OUTER_BOUND ( 'NONE', #11662, .T. ) ;
#3967=DIRECTION ( 'NONE',  ( 1.000000000000000000, 0.000000000000000000, 0.000000000000000000 ) ) ;
#4000=CYLINDRICAL_SURFACE ( 'NONE', #19075, 120.0000000000000426 ) ;
#4011=PRODUCT_DEFINITION ( 'UNKNOWN', '', #14538, #2101 ) ;
#4017=DIRECTION ( 'NONE',  ( -0.000000000000000000, -1.000000000000000000, -0.000000000000000000 ) ) ;
#4032=ORIENTED_EDGE ( 'NONE', *, *, #1933, .F. ) ;
#4051=AXIS2_PLACEMENT_3D ( 'NONE', #18764, #13999, #8907 ) ;
#4062=AXIS2_PLACEMENT_3D ( 'NONE', #11691, #13336, #6178 ) ;
#4063=ORIENTED_EDGE ( 'NONE', *, *, #8257, .F. ) ;
#4114=ADVANCED_FACE ( 'NONE', ( #21675 ), #3221, .F. ) ;
#4151=TOROIDAL_SURFACE ( 'NONE', #20040, 101.1000000000000369, 1.100000000000002087 ) ;
#4157=DIRECTION ( 'NONE',  ( 0.000000000000000000, 0.000000000000000000, 1.000000000000000000 ) ) ;
#4218=DIRECTION ( 'NONE',  ( 1.000000000000000000, 0.000000000000000000, 0.000000000000000000 ) ) ;
#4258=ORIENTED_EDGE ( 'NONE', *, *, #3245, .T. ) ;
#4273=ORIENTED_EDGE ( 'NONE', *, *, #2825, .T. ) ;
#4286=COLOUR_RGB ( '', 0.08235294, 0.09019608, 0.10196078) ;
#4310=DIRECTION ( 'NONE',  ( 0.000000000000000000, 0.000000000000000000, -1.000000000000000000 ) ) ;
#4323=EDGE_CURVE ( 'NONE', #14098, #7892, #19353, .T. ) ;
#4342=DIRECTION ( 'NONE',  ( 1.000000000000000000, 0.000000000000000000, 0.000000000000000000 ) ) ;
#4389=EDGE_LOOP ( 'NONE', ( #9965, #7681 ) ) ;
#4394=ORIENTED_EDGE ( 'NONE', *, *, #2825, .F. ) ;
#4403=CIRCLE ( 'NONE', #13926, 113.8250000000000171 ) ;
#4454=CARTESIAN_POINT ( 'NONE',  ( -90.00000000000000000, 1.393954219129474843E-14, 113.8250000000000028 ) ) ;
#4476=( NAMED_UNIT ( * ) PLANE_ANGLE_UNIT ( ) SI_UNIT ( $, .RADIAN. ) );
#4501=DIRECTION ( 'NONE',  ( 0.000000000000000000, 0.000000000000000000, -1.000000000000000000 ) ) ;
#4523=CIRCLE ( 'NONE', #21800, 105.0992000000000104 ) ;
#4541=DIRECTION ( 'NONE',  ( 1.000000000000000000, 0.000000000000000000, 0.000000000000000000 ) ) ;
#4586=ORIENTED_EDGE ( 'NONE', *, *, #1933, .T. ) ;
#4604=EDGE_CURVE ( 'NONE', #3351, #5871, #17233, .T. ) ;
#4613=EDGE_LOOP ( 'NONE', ( #4063, #21833 ) ) ;
#4638=ORIENTED_EDGE ( 'NONE', *, *, #13801, .F. ) ;
#4646=DIRECTION ( 'NONE',  ( 0.000000000000000000, 0.000000000000000000, -1.000000000000000000 ) ) ;
#4686=ADVANCED_FACE ( 'NONE', ( #7289 ), #12245, .F. ) ;
#4711=AXIS2_PLACEMENT_3D ( 'NONE', #13167, #18274, #1361 ) ;
#4729=DIRECTION ( 'NONE',  ( 0.000000000000000000, 0.000000000000000000, -1.000000000000000000 ) ) ;
#4785=CARTESIAN_POINT ( 'NONE',  ( -7.440711023145909486, 0.000000000000000000, 0.000000000000000000 ) ) ;
#4803=ORIENTED_EDGE ( 'NONE', *, *, #1939, .F. ) ;
#4816=FACE_OUTER_BOUND ( 'NONE', #9999, .T. ) ;
#4818=UNCERTAINTY_MEASURE_WITH_UNIT (LENGTH_MEASURE( 1.000000000000000082E-05 ), #2589, 'distance_accuracy_value', 'NONE');
#4820=ORIENTED_EDGE ( 'NONE', *, *, #12687, .F. ) ;
#4863=ADVANCED_FACE ( 'NONE', ( #7820 ), #753, .T. ) ;
#4893=CARTESIAN_POINT ( 'NONE',  ( 9.999999999999996447, 1.238117913937974620E-14, 101.1000000000000512 ) ) ;
#4909=DIRECTION ( 'NONE',  ( 0.000000000000000000, 0.000000000000000000, -1.000000000000000000 ) ) ;
#4915=AXIS2_PLACEMENT_3D ( 'NONE', #13684, #20436, #17110 ) ;
#4916=DIRECTION ( 'NONE',  ( 0.000000000000000000, 0.000000000000000000, -1.000000000000000000 ) ) ;
#4917=PRODUCT_DEFINITION_SHAPE ( 'NONE', 'NONE',  #4011 ) ;
#4924=EDGE_LOOP ( 'NONE', ( #21070, #16187, #10783, #4638 ) ) ;
#4947=ORIENTED_EDGE ( 'NONE', *, *, #2788, .F. ) ;
#4962=CARTESIAN_POINT ( 'NONE',  ( 9.999999999999980460, 0.000000000000000000, 0.000000000000000000 ) ) ;
#5029=DIRECTION ( 'NONE',  ( 1.000000000000000000, 0.000000000000000000, 0.000000000000000000 ) ) ;
#5037=CYLINDRICAL_SURFACE ( 'NONE', #17153, 104.9000000000000341 ) ;
#5149=CARTESIAN_POINT ( 'NONE',  ( -8.900000000000012790, 0.000000000000000000, -101.1000000000000369 ) ) ;
#5190=DIRECTION ( 'NONE',  ( -0.000000000000000000, 0.000000000000000000, 1.000000000000000000 ) ) ;
#5194=ORIENTED_EDGE ( 'NONE', *, *, #21182, .T. ) ;
#5209=VERTEX_POINT ( 'NONE', #6351 ) ;
#5230=AXIS2_PLACEMENT_3D ( 'NONE', #14628, #3029, #4909 ) ;
#5232=ORIENTED_EDGE ( 'NONE', *, *, #2761, .F. ) ;
#5242=ORIENTED_EDGE ( 'NONE', *, *, #9355, .T. ) ;
#5268=LINE ( 'NONE', #21834, #16571 ) ;
#5271=CARTESIAN_POINT ( 'NONE',  ( -10.00000000000002309, 1.462840601581513364E-14, 118.9000000000000199 ) ) ;
#5276=ORIENTED_EDGE ( 'NONE', *, *, #15864, .T. ) ;
#5306=VERTEX_POINT ( 'NONE', #2565 ) ;
#5319=DIRECTION ( 'NONE',  ( 0.000000000000000000, 1.000000000000000000, -1.224646799147353207E-16 ) ) ;
#5332=CARTESIAN_POINT ( 'NONE',  ( 9.999999999999980460, 1.393954219129475159E-14, 113.8250000000000171 ) ) ;
#5338=CARTESIAN_POINT ( 'NONE',  ( 8.899999999999991473, 0.000000000000000000, -100.0000000000000284 ) ) ;
#5376=DIRECTION ( 'NONE',  ( 0.000000000000000000, 0.000000000000000000, -1.000000000000000000 ) ) ;
#5384=CONICAL_SURFACE ( 'NONE', #21263, 103.6249999999999716, 0.5675376247847775391 ) ;
#5431=ORIENTED_EDGE ( 'NONE', *, *, #15011, .T. ) ;
#5439=DIRECTION ( 'NONE',  ( 0.000000000000000000, -1.000000000000000000, 0.000000000000000000 ) ) ;
#5446=EDGE_LOOP ( 'NONE', ( #20699, #3931, #20285, #7742 ) ) ;
#5459=VERTEX_POINT ( 'NONE', #4893 ) ;
#5478=ORIENTED_EDGE ( 'NONE', *, *, #19343, .T. ) ;
#5545=DIRECTION ( 'NONE',  ( 0.000000000000000000, 0.000000000000000000, -1.000000000000000000 ) ) ;
#5582=CIRCLE ( 'NONE', #12988, 101.1000000000000512 ) ;
#5584=VERTEX_POINT ( 'NONE', #15367 ) ;
#5601=VERTEX_POINT ( 'NONE', #5332 ) ;
#5627=CARTESIAN_POINT ( 'NONE',  ( 9.999999999999996447, 0.000000000000000000, -101.1000000000000512 ) ) ;
#5662=EDGE_CURVE ( 'NONE', #1841, #16217, #3266, .T. ) ;
#5666=FACE_OUTER_BOUND ( 'NONE', #7711, .T. ) ;
#5681=DIRECTION ( 'NONE',  ( 0.000000000000000000, -1.000000000000000000, 0.000000000000000000 ) ) ;
#5683=ADVANCED_FACE ( 'NONE', ( #21004 ), #5384, .T. ) ;
#5698=EDGE_CURVE ( 'NONE', #6130, #14098, #11019, .T. ) ;
#5704=ORIENTED_EDGE ( 'NONE', *, *, #19566, .T. ) ;
#5706=DIRECTION ( 'NONE',  ( 1.000000000000000000, -0.000000000000000000, -0.000000000000000000 ) ) ;
#5734=DIRECTION ( 'NONE',  ( 0.000000000000000000, 0.000000000000000000, -1.000000000000000000 ) ) ;
#5764=DIRECTION ( 'NONE',  ( 1.000000000000000000, -0.000000000000000000, -0.000000000000000000 ) ) ;
#5785=CARTESIAN_POINT ( 'NONE',  ( -90.00000000000000000, 0.000000000000000000, 0.000000000000000000 ) ) ;
#5812=VECTOR ( 'NONE', #17400, 1000.000000000000000 ) ;
#5815=ADVANCED_FACE ( 'NONE', ( #11935 ), #19858, .T. ) ;
#5848=DIRECTION ( 'NONE',  ( 1.000000000000000000, -0.000000000000000000, -0.000000000000000000 ) ) ;
#5871=VERTEX_POINT ( 'NONE', #13253 ) ;
#5911=EDGE_LOOP ( 'NONE', ( #12533, #7597 ) ) ;
#5914=CARTESIAN_POINT ( 'NONE',  ( 7.599999999999998757, 1.287093988729475069E-14, 105.0992000000000104 ) ) ;
#5946=ORIENTED_EDGE ( 'NONE', *, *, #7312, .F. ) ;
#5948=VERTEX_POINT ( 'NONE', #3426 ) ;
#5962=DIRECTION ( 'NONE',  ( -1.000000000000000000, -0.000000000000000000, -0.000000000000000000 ) ) ;
#5969=EDGE_CURVE ( 'NONE', #5459, #13007, #12092, .T. ) ;
#5988=DIRECTION ( 'NONE',  ( 1.000000000000000000, 0.000000000000000000, 0.000000000000000000 ) ) ;
#6022=CARTESIAN_POINT ( 'NONE',  ( -10.00000000000000888, 0.000000000000000000, 0.000000000000000000 ) ) ;
#6035=VERTEX_POINT ( 'NONE', #17124 ) ;
#6044=DIRECTION ( 'NONE',  ( 0.8432271980573223802, 6.583178742724987957E-17, 0.5375573387615476539 ) ) ;
#6063=ORIENTED_EDGE ( 'NONE', *, *, #16255, .T. ) ;
#6091=CARTESIAN_POINT ( 'NONE',  ( 7.440711023145912151, 0.000000000000000000, 0.000000000000000000 ) ) ;
#6092=DIRECTION ( 'NONE',  ( 1.000000000000000000, -0.000000000000000000, -0.000000000000000000 ) ) ;
#6130=VERTEX_POINT ( 'NONE', #16227 ) ;
#6141=ORIENTED_EDGE ( 'NONE', *, *, #1539, .F. ) ;
#6153=DIRECTION ( 'NONE',  ( 0.000000000000000000, 0.000000000000000000, -1.000000000000000000 ) ) ;
#6164=PLANE ( 'NONE',  #14369 ) ;
#6165=ORIENTED_EDGE ( 'NONE', *, *, #856, .T. ) ;
#6167=DIRECTION ( 'NONE',  ( 0.000000000000000000, 0.000000000000000000, -1.000000000000000000 ) ) ;
#6178=DIRECTION ( 'NONE',  ( 0.000000000000000000, 0.000000000000000000, -1.000000000000000000 ) ) ;
#6179=CARTESIAN_POINT ( 'NONE',  ( 8.899999999999987921, 0.000000000000000000, 0.000000000000000000 ) ) ;
#6225=CARTESIAN_POINT ( 'NONE',  ( -90.00000000000000000, 0.000000000000000000, 0.000000000000000000 ) ) ;
#6272=CARTESIAN_POINT ( 'NONE',  ( -90.00000000000000000, 0.000000000000000000, -113.8250000000000028 ) ) ;
#6308=DIRECTION ( 'NONE',  ( 0.000000000000000000, 0.000000000000000000, -1.000000000000000000 ) ) ;
#6310=CARTESIAN_POINT ( 'NONE',  ( -8.000000000000014211, 115.1000000000000227, 0.000000000000000000 ) ) ;
#6342=EDGE_LOOP ( 'NONE', ( #20723, #16642, #12648, #21609 ) ) ;
#6349=LINE ( 'NONE', #4454, #9661 ) ;
#6351=CARTESIAN_POINT ( 'NONE',  ( -8.000000000000007105, 1.284654492305574008E-14, 104.9000000000000341 ) ) ;
#6360=EDGE_LOOP ( 'NONE', ( #7528, #6502, #14661, #4947 ) ) ;
#6366=EDGE_CURVE ( 'NONE', #15511, #5306, #12824, .T. ) ;
#6394=ORIENTED_EDGE ( 'NONE', *, *, #1887, .F. ) ;
#6441=CARTESIAN_POINT ( 'NONE',  ( 8.899999999999987921, 1.456105044186203057E-14, 118.9000000000000199 ) ) ;
#6476=CIRCLE ( 'NONE', #8230, 100.0000000000000284 ) ;
#6478=ADVANCED_BREP_SHAPE_REPRESENTATION ( '', ( #20339, #15567 ), #14522 ) ;
#6500=EDGE_CURVE ( 'NONE', #19369, #10257, #20244, .T. ) ;
#6502=ORIENTED_EDGE ( 'NONE', *, *, #5969, .T. ) ;
#6514=EDGE_CURVE ( 'NONE', #14098, #13007, #2499, .T. ) ;
#6525=AXIS2_PLACEMENT_3D ( 'NONE', #5785, #12507, #19259 ) ;
#6594=DIRECTION ( 'NONE',  ( 0.000000000000000000, 1.224646799147322392E-16, 1.000000000000000000 ) ) ;
#6647=DIRECTION ( 'NONE',  ( 0.000000000000000000, 0.000000000000000000, -1.000000000000000000 ) ) ;
#6670=EDGE_CURVE ( 'NONE', #19369, #17019, #1605, .T. ) ;
#6680=DIRECTION ( 'NONE',  ( 0.000000000000000000, 0.000000000000000000, -1.000000000000000000 ) ) ;
#6695=ORIENTED_EDGE ( 'NONE', *, *, #8946, .T. ) ;
#6744=ORIENTED_EDGE ( 'NONE', *, *, #7312, .T. ) ;
#6795=CARTESIAN_POINT ( 'NONE',  ( -8.900000000000019895, 0.000000000000000000, 0.000000000000000000 ) ) ;
#6818=ADVANCED_FACE ( 'NONE', ( #17296 ), #13756, .T. ) ;
#6827=ORIENTED_EDGE ( 'NONE', *, *, #21182, .F. ) ;
#6838=AXIS2_PLACEMENT_3D ( 'NONE', #6179, #20976, #11251 ) ;
#6849=FACE_BOUND ( 'NONE', #8128, .T. ) ;
#6853=EDGE_LOOP ( 'NONE', ( #14851, #5704, #3270, #11015 ) ) ;
#6857=CARTESIAN_POINT ( 'NONE',  ( -8.900000000000012790, 0.000000000000000000, 0.000000000000000000 ) ) ;
#6862=TOROIDAL_SURFACE ( 'NONE', #3331, 105.0992000000000104, 0.2041999999999998816 ) ;
#6888=DIRECTION ( 'NONE',  ( 1.000000000000000000, 0.000000000000000000, 0.000000000000000000 ) ) ;
#6947=CARTESIAN_POINT ( 'NONE',  ( 7.999999999999979572, 1.393954219129475159E-14, 113.8250000000000171 ) ) ;
#6957=DIRECTION ( 'NONE',  ( 1.000000000000000000, 0.000000000000000000, 0.000000000000000000 ) ) ;
#6963=AXIS2_PLACEMENT_3D ( 'NONE', #889, #16140, #4310 ) ;
#6974=VECTOR ( 'NONE', #17654, 1000.000000000000000 ) ;
#6979=CARTESIAN_POINT ( 'NONE',  ( -8.900000000000018119, 1.456105044186203057E-14, 118.9000000000000199 ) ) ;
#6993=CARTESIAN_POINT ( 'NONE',  ( 7.999999999999979572, 0.000000000000000000, 0.000000000000000000 ) ) ;
#7032=EDGE_LOOP ( 'NONE', ( #9905, #17663, #19258, #18570 ) ) ;
#7044=ORIENTED_EDGE ( 'NONE', *, *, #2485, .T. ) ;
#7052=CARTESIAN_POINT ( 'NONE',  ( -7.440711023145607506, 0.000000000000000000, -115.1000000000000227 ) ) ;
#7056=CARTESIAN_POINT ( 'NONE',  ( 7.599999999999998757, 0.000000000000000000, 0.000000000000000000 ) ) ;
#7074=ORIENTED_EDGE ( 'NONE', *, *, #12306, .F. ) ;
#7081=DIRECTION ( 'NONE',  ( 0.000000000000000000, 1.000000000000000000, -1.224646799147353207E-16 ) ) ;
#7095=ORIENTED_EDGE ( 'NONE', *, *, #3235, .F. ) ;
#7097=EDGE_LOOP ( 'NONE', ( #10339, #8073, #3917, #17088 ) ) ;
#7107=DIRECTION ( 'NONE',  ( 0.000000000000000000, 0.000000000000000000, -1.000000000000000000 ) ) ;
#7123=DIRECTION ( 'NONE',  ( 1.000000000000000000, 0.000000000000000000, 0.000000000000000000 ) ) ;
#7126=DIRECTION ( 'NONE',  ( 0.000000000000000000, 0.000000000000000000, -1.000000000000000000 ) ) ;
#7127=ORIENTED_EDGE ( 'NONE', *, *, #9012, .T. ) ;
#7153=DIRECTION ( 'NONE',  ( 1.000000000000000000, 0.000000000000000000, 0.000000000000000000 ) ) ;
#7170=TOROIDAL_SURFACE ( 'NONE', #6838, 118.9000000000000199, 1.100000000000015854 ) ;
#7205=CARTESIAN_POINT ( 'NONE',  ( -7.600000000000001421, 1.287093988729475069E-14, 105.0992000000000104 ) ) ;
#7233=DIRECTION ( 'NONE',  ( 1.000000000000000000, 0.000000000000000000, 0.000000000000000000 ) ) ;
#7269=ORIENTED_EDGE ( 'NONE', *, *, #2343, .F. ) ;
#7289=FACE_OUTER_BOUND ( 'NONE', #3151, .T. ) ;
#7312=EDGE_CURVE ( 'NONE', #8212, #18019, #12510, .T. ) ;
#7315=EDGE_CURVE ( 'NONE', #7892, #13441, #13227, .T. ) ;
#7324=CARTESIAN_POINT ( 'NONE',  ( -90.00000000000000000, 0.000000000000000000, 0.000000000000000000 ) ) ;
#7339=EDGE_LOOP ( 'NONE', ( #4586, #4273 ) ) ;
#7354=ORIENTED_EDGE ( 'NONE', *, *, #8157, .T. ) ;
#7398=CARTESIAN_POINT ( 'NONE',  ( -90.00000000000000000, 0.000000000000000000, 0.000000000000000000 ) ) ;
#7402=DIRECTION ( 'NONE',  ( 1.000000000000000000, 0.000000000000000000, 0.000000000000000000 ) ) ;
#7410=ORIENTED_EDGE ( 'NONE', *, *, #7828, .F. ) ;
#7427=DIRECTION ( 'NONE',  ( 0.000000000000000000, 1.000000000000000000, -1.224646799147353207E-16 ) ) ;
#7456=VERTEX_POINT ( 'NONE', #14350 ) ;
#7473=CARTESIAN_POINT ( 'NONE',  ( 7.599999999999998757, 0.000000000000000000, 0.000000000000000000 ) ) ;
#7475=EDGE_CURVE ( 'NONE', #5601, #5584, #91, .T. ) ;
#7479=ADVANCED_FACE ( 'NONE', ( #1314 ), #14198, .T. ) ;
#7497=DIRECTION ( 'NONE',  ( 0.000000000000000000, 0.000000000000000000, -1.000000000000000000 ) ) ;
#7528=ORIENTED_EDGE ( 'NONE', *, *, #2710, .T. ) ;
#7530=CIRCLE ( 'NONE', #2941, 100.0000000000000284 ) ;
#7558=CIRCLE ( 'NONE', #11440, 120.0000000000000284 ) ;
#7560=AXIS2_PLACEMENT_3D ( 'NONE', #11299, #18048, #9620 ) ;
#7585=DIRECTION ( 'NONE',  ( 0.000000000000000000, 0.000000000000000000, -1.000000000000000000 ) ) ;
#7591=AXIS2_PLACEMENT_3D ( 'NONE', #212, #6957, #16093 ) ;
#7593=LINE ( 'NONE', #11126, #6974 ) ;
#7597=ORIENTED_EDGE ( 'NONE', *, *, #18368, .F. ) ;
#7612=DIRECTION ( 'NONE',  ( 0.000000000000000000, 0.000000000000000000, 1.000000000000000000 ) ) ;
#7624=AXIS2_PLACEMENT_3D ( 'NONE', #9098, #15849, #708 ) ;
#7679=AXIS2_PLACEMENT_3D ( 'NONE', #3450, #18153, #9733 ) ;
#7681=ORIENTED_EDGE ( 'NONE', *, *, #20558, .T. ) ;
#7697=FACE_OUTER_BOUND ( 'NONE', #5911, .T. ) ;
#7711=EDGE_LOOP ( 'NONE', ( #12257, #18137, #1812, #20675 ) ) ;
#7742=ORIENTED_EDGE ( 'NONE', *, *, #9594, .F. ) ;
#7789=CARTESIAN_POINT ( 'NONE',  ( 8.899999999999989697, 0.000000000000000000, 0.000000000000000000 ) ) ;
#7802=CARTESIAN_POINT ( 'NONE',  ( -90.00000000000000000, 1.224646799147353533E-14, 100.0000000000000284 ) ) ;
#7806=DIRECTION ( 'NONE',  ( -1.000000000000000000, 0.000000000000000000, 0.000000000000000000 ) ) ;
#7812=FACE_OUTER_BOUND ( 'NONE', #1481, .T. ) ;
#7820=FACE_OUTER_BOUND ( 'NONE', #20027, .T. ) ;
#7828=EDGE_CURVE ( 'NONE', #14098, #6130, #6476, .T. ) ;
#7837=AXIS2_PLACEMENT_3D ( 'NONE', #18027, #4541, #4646 ) ;
#7845=CARTESIAN_POINT ( 'NONE',  ( 9.999999999999994671, 0.000000000000000000, 0.000000000000000000 ) ) ;
#7852=LINE ( 'NONE', #9831, #11534 ) ;
#7872=CARTESIAN_POINT ( 'NONE',  ( 8.899999999999991473, 0.000000000000000000, 0.000000000000000000 ) ) ;
#7891=VECTOR ( 'NONE', #14536, 1000.000000000000000 ) ;
#7892=VERTEX_POINT ( 'NONE', #8868 ) ;
#7941=AXIS2_PLACEMENT_3D ( 'NONE', #3288, #3402, #20197 ) ;
#7945=DIRECTION ( 'NONE',  ( 1.000000000000000000, 0.000000000000000000, 0.000000000000000000 ) ) ;
#7955=CIRCLE ( 'NONE', #21362, 0.2042000000000016025 ) ;
#7969=ORIENTED_EDGE ( 'NONE', *, *, #3245, .F. ) ;
#7973=CIRCLE ( 'NONE', #19981, 0.2042000000000016025 ) ;
#7974=ORIENTED_EDGE ( 'NONE', *, *, #17837, .F. ) ;
#7979=EDGE_LOOP ( 'NONE', ( #17854, #17461, #13010, #13718 ) ) ;
#8029=ORIENTED_EDGE ( 'NONE', *, *, #1093, .F. ) ;
#8033=ORIENTED_EDGE ( 'NONE', *, *, #15656, .T. ) ;
#8058=DIRECTION ( 'NONE',  ( 1.000000000000000000, 0.000000000000000000, 0.000000000000000000 ) ) ;
#8073=ORIENTED_EDGE ( 'NONE', *, *, #6500, .T. ) ;
#8079=VECTOR ( 'NONE', #2832, 1000.000000000000000 ) ;
#8089=VERTEX_POINT ( 'NONE', #12728 ) ;
#8128=EDGE_LOOP ( 'NONE', ( #18421, #15143 ) ) ;
#8157=EDGE_CURVE ( 'NONE', #3216, #13007, #7530, .T. ) ;
#8161=DIRECTION ( 'NONE',  ( 0.000000000000000000, 0.000000000000000000, -1.000000000000000000 ) ) ;
#8212=VERTEX_POINT ( 'NONE', #15206 ) ;
#8220=( NAMED_UNIT ( * ) SI_UNIT ( $, .STERADIAN. ) SOLID_ANGLE_UNIT ( ) );
#8230=AXIS2_PLACEMENT_3D ( 'NONE', #6795, #18502, #3355 ) ;
#8255=EDGE_CURVE ( 'NONE', #18016, #15663, #485, .T. ) ;
#8257=EDGE_CURVE ( 'NONE', #12158, #2019, #10351, .T. ) ;
#8310=EDGE_LOOP ( 'NONE', ( #7269, #6695, #13080, #1763 ) ) ;
#8312=EDGE_LOOP ( 'NONE', ( #2320, #15064, #14993, #7074 ) ) ;
#8316=FACE_OUTER_BOUND ( 'NONE', #14243, .T. ) ;
#8332=VECTOR ( 'NONE', #20462, 1000.000000000000000 ) ;
#8349=CARTESIAN_POINT ( 'NONE',  ( -7.440711023145909486, 1.285874240517524538E-14, 104.9000000000000341 ) ) ;
#8370=ORIENTED_EDGE ( 'NONE', *, *, #1796, .F. ) ;
#8378=DIRECTION ( 'NONE',  ( 1.000000000000000000, -0.000000000000000000, -0.000000000000000000 ) ) ;
#8388=CIRCLE ( 'NONE', #11202, 0.2042000000000016025 ) ;
#8391=SURFACE_SIDE_STYLE ('',( #13795 ) ) ;
#8401=DIRECTION ( 'NONE',  ( 0.000000000000000000, 1.000000000000000000, -1.224646799147353207E-16 ) ) ;
#8448=CIRCLE ( 'NONE', #20776, 100.0000000000000284 ) ;
#8466=TOROIDAL_SURFACE ( 'NONE', #10927, 101.1000000000000512, 1.100000000000009859 ) ;
#8517=ADVANCED_FACE ( 'NONE', ( #12755 ), #3321, .T. ) ;
#8520=ADVANCED_FACE ( 'NONE', ( #1280 ), #8960, .T. ) ;
#8522=ORIENTED_EDGE ( 'NONE', *, *, #3411, .F. ) ;
#8542=ADVANCED_FACE ( 'NONE', ( #9648 ), #18847, .T. ) ;
#8589=CIRCLE ( 'NONE', #20933, 115.1000000000000227 ) ;
#8667=DIRECTION ( 'NONE',  ( 1.000000000000000000, 0.000000000000000000, 0.000000000000000000 ) ) ;
#8692=CARTESIAN_POINT ( 'NONE',  ( 7.440711023145912151, 0.000000000000000000, 0.000000000000000000 ) ) ;
#8701=DIRECTION ( 'NONE',  ( 0.000000000000000000, 0.000000000000000000, -1.000000000000000000 ) ) ;
#8704=FACE_OUTER_BOUND ( 'NONE', #8310, .T. ) ;
#8752=DIRECTION ( 'NONE',  ( 1.000000000000000000, 0.000000000000000000, 0.000000000000000000 ) ) ;
#8761=ORIENTED_EDGE ( 'NONE', *, *, #3783, .T. ) ;
#8786=CARTESIAN_POINT ( 'NONE',  ( 8.000000000000007105, 0.000000000000000000, -104.9000000000000341 ) ) ;
#8808=VECTOR ( 'NONE', #16185, 1000.000000000000000 ) ;
#8839=CARTESIAN_POINT ( 'NONE',  ( -7.440711023145909486, 0.000000000000000000, 0.000000000000000000 ) ) ;
#8842=CARTESIAN_POINT ( 'NONE',  ( 9.999999999999994671, 0.000000000000000000, 103.6249999999999716 ) ) ;
#8858=DIRECTION ( 'NONE',  ( 0.000000000000000000, -1.000000000000000000, 0.000000000000000000 ) ) ;
#8862=DIRECTION ( 'NONE',  ( 1.000000000000000000, 0.000000000000000000, 0.000000000000000000 ) ) ;
#8868=CARTESIAN_POINT ( 'NONE',  ( -10.00000000000001243, 1.238117913937974462E-14, 101.1000000000000369 ) ) ;
#8880=DIRECTION ( 'NONE',  ( 1.000000000000000000, 0.000000000000000000, 0.000000000000000000 ) ) ;
#8887=ADVANCED_FACE ( 'NONE', ( #20706 ), #14167, .F. ) ;
#8901=AXIS2_PLACEMENT_3D ( 'NONE', #2538, #6092, #15917 ) ;
#8907=DIRECTION ( 'NONE',  ( 0.000000000000000000, 0.000000000000000000, -1.000000000000000000 ) ) ;
#8910=ORIENTED_EDGE ( 'NONE', *, *, #16516, .T. ) ;
#8946=EDGE_CURVE ( 'NONE', #5948, #16620, #6349, .T. ) ;
#8960=TOROIDAL_SURFACE ( 'NONE', #14244, 118.9000000000000199, 1.100000000000009859 ) ;
#8985=CARTESIAN_POINT ( 'NONE',  ( 8.899999999999989697, 0.000000000000000000, -101.1000000000000512 ) ) ;
#9007=CARTESIAN_POINT ( 'NONE',  ( -10.00000000000001243, 103.6250000000000284, 0.000000000000000000 ) ) ;
#9012=EDGE_CURVE ( 'NONE', #5871, #3351, #153, .T. ) ;
#9035=CARTESIAN_POINT ( 'NONE',  ( -90.00000000000000000, 0.000000000000000000, 0.000000000000000000 ) ) ;
#9041=EDGE_CURVE ( 'NONE', #9325, #5584, #13902, .T. ) ;
#9070=CARTESIAN_POINT ( 'NONE',  ( 8.899999999999991473, 1.469576158976824618E-14, 120.0000000000000711 ) ) ;
#9076=AXIS2_PLACEMENT_3D ( 'NONE', #13176, #11649, #21375 ) ;
#9082=ORIENTED_EDGE ( 'NONE', *, *, #1887, .T. ) ;
#9098=CARTESIAN_POINT ( 'NONE',  ( -7.395800000000001262, 0.000000000000000000, -105.0992000000000104 ) ) ;
#9130=AXIS2_PLACEMENT_3D ( 'NONE', #6979, #5319, #12045 ) ;
#9133=FACE_BOUND ( 'NONE', #1919, .T. ) ;
#9140=ADVANCED_FACE ( 'NONE', ( #8316 ), #2638, .T. ) ;
#9147=CARTESIAN_POINT ( 'NONE',  ( -10.00000000000002309, 0.000000000000000000, 0.000000000000000000 ) ) ;
#9153=DIRECTION ( 'NONE',  ( 1.000000000000000000, -0.000000000000000000, -0.000000000000000000 ) ) ;
#9179=FACE_OUTER_BOUND ( 'NONE', #14977, .T. ) ;
#9208=ADVANCED_FACE ( 'NONE', ( #12681 ), #20864, .F. ) ;
#9216=ADVANCED_FACE ( 'NONE', ( #14345 ), #1583, .T. ) ;
#9221=ORIENTED_EDGE ( 'NONE', *, *, #21343, .F. ) ;
#9222=FACE_OUTER_BOUND ( 'NONE', #11517, .T. ) ;
#9242=DIRECTION ( 'NONE',  ( 1.000000000000000000, 0.000000000000000000, 0.000000000000000000 ) ) ;
#9290=EDGE_CURVE ( 'NONE', #1656, #5948, #11115, .T. ) ;
#9296=AXIS2_PLACEMENT_3D ( 'NONE', #21269, #16290, #18300 ) ;
#9311=VECTOR ( 'NONE', #6044, 1000.000000000000227 ) ;
#9322=ORIENTED_EDGE ( 'NONE', *, *, #20647, .F. ) ;
#9325=VERTEX_POINT ( 'NONE', #16110 ) ;
#9355=EDGE_CURVE ( 'NONE', #19336, #993, #19236, .T. ) ;
#9364=AXIS2_PLACEMENT_3D ( 'NONE', #10317, #7123, #17393 ) ;
#9374=VECTOR ( 'NONE', #19645, 1000.000000000000000 ) ;
#9392=ORIENTED_EDGE ( 'NONE', *, *, #12177, .F. ) ;
#9403=EDGE_CURVE ( 'NONE', #20730, #3351, #18215, .T. ) ;
#9471=CIRCLE ( 'NONE', #20443, 103.6249999999999716 ) ;
#9489=ORIENTED_EDGE ( 'NONE', *, *, #13068, .T. ) ;
#9515=EDGE_LOOP ( 'NONE', ( #20442, #18024, #11219, #15637 ) ) ;
#9516=ORIENTED_EDGE ( 'NONE', *, *, #9708, .T. ) ;
#9536=FACE_OUTER_BOUND ( 'NONE', #6853, .T. ) ;
#9543=DIRECTION ( 'NONE',  ( 0.000000000000000000, 0.000000000000000000, -1.000000000000000000 ) ) ;
#9556=DIRECTION ( 'NONE',  ( 1.000000000000000000, 0.000000000000000000, -0.000000000000000000 ) ) ;
#9594=EDGE_CURVE ( 'NONE', #20730, #21817, #7558, .T. ) ;
#9620=DIRECTION ( 'NONE',  ( 0.000000000000000000, 0.000000000000000000, -1.000000000000000000 ) ) ;
#9648=FACE_OUTER_BOUND ( 'NONE', #15203, .T. ) ;
#9650=EDGE_LOOP ( 'NONE', ( #7410, #13749, #5478, #8522 ) ) ;
#9658=UNCERTAINTY_MEASURE_WITH_UNIT (LENGTH_MEASURE( 1.000000000000000082E-05 ), #10091, 'distance_accuracy_value', 'NONE');
#9661=VECTOR ( 'NONE', #21573, 1000.000000000000000 ) ;
#9662=DIRECTION ( 'NONE',  ( -0.000000000000000000, 0.000000000000000000, 1.000000000000000000 ) ) ;
#9708=EDGE_CURVE ( 'NONE', #2019, #5209, #15641, .T. ) ;
#9733=DIRECTION ( 'NONE',  ( 0.000000000000000000, 0.000000000000000000, -1.000000000000000000 ) ) ;
#9752=ADVANCED_FACE ( 'NONE', ( #9222 ), #6862, .T. ) ;
#9765=DIRECTION ( 'NONE',  ( 0.000000000000000000, 0.000000000000000000, -1.000000000000000000 ) ) ;
#9776=CARTESIAN_POINT ( 'NONE',  ( -8.900000000000019895, 0.000000000000000000, 0.000000000000000000 ) ) ;
#9791=ORIENTED_EDGE ( 'NONE', *, *, #5662, .F. ) ;
#9831=CARTESIAN_POINT ( 'NONE',  ( -90.00000000000000000, 0.000000000000000000, -100.0000000000000284 ) ) ;
#9841=ORIENTED_EDGE ( 'NONE', *, *, #14843, .T. ) ;
#9859=DIRECTION ( 'NONE',  ( -1.000000000000000000, 0.000000000000000000, 0.000000000000000000 ) ) ;
#9865=EDGE_LOOP ( 'NONE', ( #19901, #3715 ) ) ;
#9905=ORIENTED_EDGE ( 'NONE', *, *, #5698, .T. ) ;
#9909=LINE ( 'NONE', #16651, #9374 ) ;
#9918=CARTESIAN_POINT ( 'NONE',  ( 9.999999999999980460, 0.000000000000000000, 0.000000000000000000 ) ) ;
#9924=VERTEX_POINT ( 'NONE', #13753 ) ;
#9925=( NAMED_UNIT ( * ) PLANE_ANGLE_UNIT ( ) SI_UNIT ( $, .RADIAN. ) );
#9965=ORIENTED_EDGE ( 'NONE', *, *, #11342, .T. ) ;
#9966=ADVANCED_FACE ( 'NONE', ( #2036 ), #3585, .F. ) ;
#9975=( NAMED_UNIT ( * ) SI_UNIT ( $, .STERADIAN. ) SOLID_ANGLE_UNIT ( ) );
#9999=EDGE_LOOP ( 'NONE', ( #17024, #2621, #14830, #14444 ) ) ;
#10024=VECTOR ( 'NONE', #5029, 1000.000000000000000 ) ;
#10057=TOROIDAL_SURFACE ( 'NONE', #10405, 118.9000000000000199, 1.100000000000009859 ) ;
#10091=( LENGTH_UNIT ( ) NAMED_UNIT ( * ) SI_UNIT ( .MILLI., .METRE. ) );
#10102=CARTESIAN_POINT ( 'NONE',  ( 10.00000000000000888, 0.000000000000000000, -118.9000000000000199 ) ) ;
#10120=CARTESIAN_POINT ( 'NONE',  ( -8.900000000000019895, 0.000000000000000000, -120.0000000000000284 ) ) ;
#10136=DIRECTION ( 'NONE',  ( 0.000000000000000000, 0.000000000000000000, -1.000000000000000000 ) ) ;
#10141=CIRCLE ( 'NONE', #9076, 115.1000000000000227 ) ;
#10148=FACE_OUTER_BOUND ( 'NONE', #21103, .T. ) ;
#10163=FACE_OUTER_BOUND ( 'NONE', #16712, .T. ) ;
#10170=ORIENTED_EDGE ( 'NONE', *, *, #6670, .F. ) ;
#10173=AXIS2_PLACEMENT_3D ( 'NONE', #12271, #17476, #18801 ) ;
#10193=( GEOMETRIC_REPRESENTATION_CONTEXT ( 3 ) GLOBAL_UNCERTAINTY_ASSIGNED_CONTEXT ( ( #1289 ) ) GLOBAL_UNIT_ASSIGNED_CONTEXT ( ( #15116, #9925, #18558 ) ) REPRESENTATION_CONTEXT ( 'NONE', 'WORKASPACE' ) );
#10239=CIRCLE ( 'NONE', #20481, 105.0992000000000104 ) ;
#10257=VERTEX_POINT ( 'NONE', #14509 ) ;
#10317=CARTESIAN_POINT ( 'NONE',  ( 7.999999999999979572, 0.000000000000000000, 0.000000000000000000 ) ) ;
#10325=DIRECTION ( 'NONE',  ( 1.000000000000000000, 0.000000000000000000, 0.000000000000000000 ) ) ;
#10328=EDGE_LOOP ( 'NONE', ( #6063, #8910 ) ) ;
#10330=DIRECTION ( 'NONE',  ( 1.000000000000000000, 0.000000000000000000, 0.000000000000000000 ) ) ;
#10339=ORIENTED_EDGE ( 'NONE', *, *, #445, .F. ) ;
#10351=CIRCLE ( 'NONE', #11055, 103.6250000000000284 ) ;
#10370=ADVANCED_FACE ( 'NONE', ( #21790, #3225 ), #1688, .T. ) ;
#10405=AXIS2_PLACEMENT_3D ( 'NONE', #2280, #19300, #17873 ) ;
#10406=EDGE_LOOP ( 'NONE', ( #9392, #13515, #3739, #18496 ) ) ;
#10453=DIRECTION ( 'NONE',  ( 0.000000000000000000, 0.000000000000000000, 1.000000000000000000 ) ) ;
#10521=CARTESIAN_POINT ( 'NONE',  ( -90.00000000000000000, 0.000000000000000000, 0.000000000000000000 ) ) ;
#10542=DIRECTION ( 'NONE',  ( 0.000000000000000000, 0.000000000000000000, -1.000000000000000000 ) ) ;
#10549=EDGE_CURVE ( 'NONE', #19408, #1529, #17475, .T. ) ;
#10560=EDGE_CURVE ( 'NONE', #5306, #15511, #1948, .T. ) ;
#10565=AXIS2_PLACEMENT_3D ( 'NONE', #140, #6888, #7107 ) ;
#10700=CARTESIAN_POINT ( 'NONE',  ( -8.000000000000007105, 0.000000000000000000, 0.000000000000000000 ) ) ;
#10726=CARTESIAN_POINT ( 'NONE',  ( -10.00000000000000888, 1.276847368961009516E-14, 103.6250000000000284 ) ) ;
#10754=AXIS2_PLACEMENT_3D ( 'NONE', #15918, #5764, #2445 ) ;
#10756=AXIS2_PLACEMENT_3D ( 'NONE', #7398, #14015, #2517 ) ;
#10760=FACE_OUTER_BOUND ( 'NONE', #7032, .T. ) ;
#10764=DIRECTION ( 'NONE',  ( 0.000000000000000000, 0.000000000000000000, -1.000000000000000000 ) ) ;
#10783=ORIENTED_EDGE ( 'NONE', *, *, #18609, .T. ) ;
#10804=CARTESIAN_POINT ( 'NONE',  ( -7.395799999999999486, 0.000000000000000000, 0.000000000000000000 ) ) ;
#10817=TOROIDAL_SURFACE ( 'NONE', #6963, 114.9007999999999896, 0.2041999999999998816 ) ;
#10827=CIRCLE ( 'NONE', #15769, 104.9000000000000341 ) ;
#10862=CIRCLE ( 'NONE', #5230, 118.9000000000000199 ) ;
#10899=CIRCLE ( 'NONE', #9130, 1.100000000000003642 ) ;
#10921=CARTESIAN_POINT ( 'NONE',  ( 9.999999999999994671, 0.000000000000000000, 0.000000000000000000 ) ) ;
#10927=AXIS2_PLACEMENT_3D ( 'NONE', #7789, #16394, #1268 ) ;
#10931=EDGE_LOOP ( 'NONE', ( #19545, #767 ) ) ;
#10932=EDGE_LOOP ( 'NONE', ( #7974, #11069, #556, #13360 ) ) ;
#10998=ORIENTED_EDGE ( 'NONE', *, *, #10549, .F. ) ;
#11007=DIRECTION ( 'NONE',  ( -0.000000000000000000, 0.000000000000000000, -1.000000000000000000 ) ) ;
#11015=ORIENTED_EDGE ( 'NONE', *, *, #18609, .F. ) ;
#11019=CIRCLE ( 'NONE', #7837, 100.0000000000000284 ) ;
#11055=AXIS2_PLACEMENT_3D ( 'NONE', #302, #13776, #5376 ) ;
#11062=CARTESIAN_POINT ( 'NONE',  ( -90.00000000000000000, 0.000000000000000000, -104.9000000000000341 ) ) ;
#11069=ORIENTED_EDGE ( 'NONE', *, *, #11342, .F. ) ;
#11071=AXIS2_PLACEMENT_3D ( 'NONE', #15945, #4017, #14286 ) ;
#11081=CARTESIAN_POINT ( 'NONE',  ( -10.00000000000000888, 0.000000000000000000, 0.000000000000000000 ) ) ;
#11097=CYLINDRICAL_SURFACE ( 'NONE', #19386, 104.9000000000000341 ) ;
#11104=DIRECTION ( 'NONE',  ( 1.000000000000000000, 0.000000000000000000, 0.000000000000000000 ) ) ;
#11115=CIRCLE ( 'NONE', #16761, 113.8250000000000028 ) ;
#11117=ADVANCED_FACE ( 'NONE', ( #4816 ), #20588, .T. ) ;
#11126=CARTESIAN_POINT ( 'NONE',  ( 9.999999999999994671, 1.269040245616444393E-14, -103.6249999999999716 ) ) ;
#11137=CLOSED_SHELL ( 'NONE', ( #11117, #20841, #3233, #18257, #12338, #19449, #16857, #8517, #20549, #9752, #16370, #4686, #4114, #694, #4863, #8520, #2284, #20173, #3146, #17436, #9208, #18795, #16631, #21207, #9140, #19623, #9966, #15623, #13620, #9216, #1142, #7479, #1762, #17839, #13397, #6818, #985, #8542, #1001, #5815, #8887, #20439, #10370, #5683 ) ) ;
#11150=DIRECTION ( 'NONE',  ( 1.000000000000000000, 0.000000000000000000, 0.000000000000000000 ) ) ;
#11176=CARTESIAN_POINT ( 'NONE',  ( -10.00000000000001954, 113.8250000000000028, 0.000000000000000000 ) ) ;
#11202=AXIS2_PLACEMENT_3D ( 'NONE', #18077, #2932, #7585 ) ;
#11205=DIRECTION ( 'NONE',  ( 0.000000000000000000, 0.000000000000000000, -1.000000000000000000 ) ) ;
#11215=AXIS2_PLACEMENT_3D ( 'NONE', #19080, #18863, #2169 ) ;
#11219=ORIENTED_EDGE ( 'NONE', *, *, #2386, .T. ) ;
#11233=AXIS2_PLACEMENT_3D ( 'NONE', #6225, #12941, #20355 ) ;
#11251=DIRECTION ( 'NONE',  ( 0.000000000000000000, 0.000000000000000000, -1.000000000000000000 ) ) ;
#11291=AXIS2_PLACEMENT_3D ( 'NONE', #6441, #20022, #3215 ) ;
#11294=EDGE_LOOP ( 'NONE', ( #5194, #18631 ) ) ;
#11299=CARTESIAN_POINT ( 'NONE',  ( 8.899999999999991473, 0.000000000000000000, 0.000000000000000000 ) ) ;
#11328=EDGE_CURVE ( 'NONE', #6130, #13441, #3306, .T. ) ;
#11342=EDGE_CURVE ( 'NONE', #1609, #17412, #20231, .T. ) ;
#11350=AXIS2_PLACEMENT_3D ( 'NONE', #3939, #17421, #2276 ) ;
#11358=AXIS2_PLACEMENT_3D ( 'NONE', #2659, #4218, #20797 ) ;
#11408=DIRECTION ( 'NONE',  ( 0.000000000000000000, 0.000000000000000000, -1.000000000000000000 ) ) ;
#11422=FACE_BOUND ( 'NONE', #12035, .T. ) ;
#11440=AXIS2_PLACEMENT_3D ( 'NONE', #1633, #13779, #15209 ) ;
#11441=EDGE_CURVE ( 'NONE', #10257, #5306, #21298, .T. ) ;
#11493=EDGE_LOOP ( 'NONE', ( #19991, #9516, #21130, #5232 ) ) ;
#11505=VERTEX_POINT ( 'NONE', #19707 ) ;
#11517=EDGE_LOOP ( 'NONE', ( #8370, #669, #6827, #2591 ) ) ;
#11534=VECTOR ( 'NONE', #16800, 1000.000000000000000 ) ;
#11569=AXIS2_PLACEMENT_3D ( 'NONE', #2600, #19292, #4157 ) ;
#11602=AXIS2_PLACEMENT_3D ( 'NONE', #20823, #8880, #7126 ) ;
#11605=CARTESIAN_POINT ( 'NONE',  ( 8.899999999999991473, 0.000000000000000000, 0.000000000000000000 ) ) ;
#11607=CARTESIAN_POINT ( 'NONE',  ( 7.395800000000001262, 1.407128969394701661E-14, 114.9007999999999896 ) ) ;
#11625=EDGE_LOOP ( 'NONE', ( #9322, #4032, #11787, #2252 ) ) ;
#11649=DIRECTION ( 'NONE',  ( 1.000000000000000000, 0.000000000000000000, 0.000000000000000000 ) ) ;
#11654=SHAPE_REPRESENTATION_RELATIONSHIP ( 'NONE' , 'NONE' ,  #16445, #6478 ) ;
#11662=EDGE_LOOP ( 'NONE', ( #7127, #3824, #17189, #7095 ) ) ;
#11663=DIRECTION ( 'NONE',  ( 0.000000000000000000, 0.000000000000000000, -1.000000000000000000 ) ) ;
#11691=CARTESIAN_POINT ( 'NONE',  ( -7.440711023145607506, 0.000000000000000000, 0.000000000000000000 ) ) ;
#11711=DIRECTION ( 'NONE',  ( 1.000000000000000000, 0.000000000000000000, 0.000000000000000000 ) ) ;
#11730=ORIENTED_EDGE ( 'NONE', *, *, #15533, .F. ) ;
#11734=FACE_OUTER_BOUND ( 'NONE', #8312, .T. ) ;
#11787=ORIENTED_EDGE ( 'NONE', *, *, #9041, .T. ) ;
#11795=DIRECTION ( 'NONE',  ( 1.000000000000000000, 0.000000000000000000, 0.000000000000000000 ) ) ;
#11797=EDGE_CURVE ( 'NONE', #2646, #1841, #7973, .T. ) ;
#11804=AXIS2_PLACEMENT_3D ( 'NONE', #490, #7233, #20498 ) ;
#11823=DIRECTION ( 'NONE',  ( 1.000000000000000000, 0.000000000000000000, 0.000000000000000000 ) ) ;
#11831=ORIENTED_EDGE ( 'NONE', *, *, #2549, .F. ) ;
#11847=CARTESIAN_POINT ( 'NONE',  ( 9.999999999999994671, 0.000000000000000000, 0.000000000000000000 ) ) ;
#11932=DIRECTION ( 'NONE',  ( 0.000000000000000000, 1.224646799147322392E-16, 1.000000000000000000 ) ) ;
#11935=FACE_OUTER_BOUND ( 'NONE', #6342, .T. ) ;
#11961=DIRECTION ( 'NONE',  ( 1.000000000000000000, 0.000000000000000000, 0.000000000000000000 ) ) ;
#12003=VERTEX_POINT ( 'NONE', #5627 ) ;
#12035=EDGE_LOOP ( 'NONE', ( #21429, #458 ) ) ;
#12045=DIRECTION ( 'NONE',  ( 0.000000000000000000, 1.224646799147368738E-16, 1.000000000000000000 ) ) ;
#12060=DIRECTION ( 'NONE',  ( 0.000000000000000000, 0.000000000000000000, -1.000000000000000000 ) ) ;
#12065=FACE_OUTER_BOUND ( 'NONE', #9650, .T. ) ;
#12092=CIRCLE ( 'NONE', #18805, 1.100000000000003642 ) ;
#12099=CARTESIAN_POINT ( 'NONE',  ( 8.899999999999991473, 0.000000000000000000, 0.000000000000000000 ) ) ;
#12108=ORIENTED_EDGE ( 'NONE', *, *, #13060, .T. ) ;
#12122=TOROIDAL_SURFACE ( 'NONE', #4711, 105.0992000000000104, 0.2042000000000007420 ) ;
#12143=CARTESIAN_POINT ( 'NONE',  ( -90.00000000000000000, 1.409568465818603827E-14, 115.1000000000000227 ) ) ;
#12158=VERTEX_POINT ( 'NONE', #13113 ) ;
#12173=FACE_OUTER_BOUND ( 'NONE', #13957, .T. ) ;
#12177=EDGE_CURVE ( 'NONE', #5209, #2646, #9909, .T. ) ;
#12183=DIRECTION ( 'NONE',  ( 1.000000000000000000, -0.000000000000000000, -0.000000000000000000 ) ) ;
#12204=CARTESIAN_POINT ( 'NONE',  ( 10.00000000000000888, 1.462840601581513680E-14, 118.9000000000000199 ) ) ;
#12245=CYLINDRICAL_SURFACE ( 'NONE', #661, 115.1000000000000227 ) ;
#12257=ORIENTED_EDGE ( 'NONE', *, *, #9403, .F. ) ;
#12271=CARTESIAN_POINT ( 'NONE',  ( -8.900000000000012790, 1.238117913937974462E-14, 101.1000000000000369 ) ) ;
#12306=EDGE_CURVE ( 'NONE', #15663, #18016, #12870, .T. ) ;
#12338=ADVANCED_FACE ( 'NONE', ( #18438 ), #19632, .T. ) ;
#12346=CARTESIAN_POINT ( 'NONE',  ( 7.395799999999999486, 0.000000000000000000, -105.0992000000000104 ) ) ;
#12372=VERTEX_POINT ( 'NONE', #6947 ) ;
#12411=LINE ( 'NONE', #496, #5812 ) ;
#12439=DIRECTION ( 'NONE',  ( -0.000000000000000000, -1.000000000000000000, -0.000000000000000000 ) ) ;
#12445=CARTESIAN_POINT ( 'NONE',  ( 8.899999999999989697, 0.000000000000000000, 0.000000000000000000 ) ) ;
#12507=DIRECTION ( 'NONE',  ( 1.000000000000000000, 0.000000000000000000, 0.000000000000000000 ) ) ;
#12510=CIRCLE ( 'NONE', #15338, 114.9007999999999896 ) ;
#12527=VERTEX_POINT ( 'NONE', #2601 ) ;
#12533=ORIENTED_EDGE ( 'NONE', *, *, #12818, .F. ) ;
#12545=PLANE ( 'NONE',  #11569 ) ;
#12623=VECTOR ( 'NONE', #599, 1000.000000000000000 ) ;
#12648=ORIENTED_EDGE ( 'NONE', *, *, #11328, .T. ) ;
#12656=DIRECTION ( 'NONE',  ( 1.000000000000000000, -0.000000000000000000, -0.000000000000000000 ) ) ;
#12681=FACE_OUTER_BOUND ( 'NONE', #9515, .T. ) ;
#12687=EDGE_CURVE ( 'NONE', #18019, #19336, #7955, .T. ) ;
#12695=FACE_BOUND ( 'NONE', #9865, .T. ) ;
#12697=EDGE_LOOP ( 'NONE', ( #6744, #3419, #5242, #19636 ) ) ;
#12707=DIRECTION ( 'NONE',  ( 0.000000000000000000, 0.000000000000000000, -1.000000000000000000 ) ) ;
#12728=CARTESIAN_POINT ( 'NONE',  ( -7.440711023145909486, 0.000000000000000000, -104.9000000000000341 ) ) ;
#12729=AXIS2_PLACEMENT_3D ( 'NONE', #9776, #13095, #21713 ) ;
#12738=CARTESIAN_POINT ( 'NONE',  ( 8.899999999999991473, 1.224646799147353533E-14, 100.0000000000000284 ) ) ;
#12755=FACE_OUTER_BOUND ( 'NONE', #7979, .T. ) ;
#12759=FACE_OUTER_BOUND ( 'NONE', #3857, .T. ) ;
#12769=DIRECTION ( 'NONE',  ( 1.000000000000000000, -0.000000000000000000, -0.000000000000000000 ) ) ;
#12791=DIRECTION ( 'NONE',  ( 0.000000000000000000, 0.000000000000000000, -1.000000000000000000 ) ) ;
#12795=ORIENTED_EDGE ( 'NONE', *, *, #16707, .T. ) ;
#12803=ORIENTED_EDGE ( 'NONE', *, *, #9355, .F. ) ;
#12818=EDGE_CURVE ( 'NONE', #12527, #17019, #13614, .T. ) ;
#12824=CIRCLE ( 'NONE', #1546, 114.9007999999999896 ) ;
#12841=LINE ( 'NONE', #20916, #12623 ) ;
#12842=DIRECTION ( 'NONE',  ( 1.000000000000000000, 0.000000000000000000, 0.000000000000000000 ) ) ;
#12870=CIRCLE ( 'NONE', #20689, 104.9000000000000341 ) ;
#12878=ORIENTED_EDGE ( 'NONE', *, *, #6670, .T. ) ;
#12938=DIRECTION ( 'NONE',  ( 0.000000000000000000, 0.000000000000000000, -1.000000000000000000 ) ) ;
#12941=DIRECTION ( 'NONE',  ( 1.000000000000000000, 0.000000000000000000, 0.000000000000000000 ) ) ;
#12968=CARTESIAN_POINT ( 'NONE',  ( -8.000000000000007105, 0.000000000000000000, -115.1000000000000227 ) ) ;
#12983=EDGE_CURVE ( 'NONE', #2019, #12158, #20333, .T. ) ;
#12988=AXIS2_PLACEMENT_3D ( 'NONE', #11847, #15487, #16941 ) ;
#13007=VERTEX_POINT ( 'NONE', #12738 ) ;
#13010=ORIENTED_EDGE ( 'NONE', *, *, #10560, .F. ) ;
#13013=CARTESIAN_POINT ( 'NONE',  ( -90.00000000000000000, 1.469576158976824302E-14, 120.0000000000000426 ) ) ;
#13017=TOROIDAL_SURFACE ( 'NONE', #16184, 105.0992000000000104, 0.2042000000000007420 ) ;
#13018=PRODUCT ( 'radial cylindrical roller bearing_iso_ISO 15 RCR - 17200 - 54,SI,NC,54', 'radial cylindrical roller bearing_iso_ISO 15 RCR - 17200 - 54,SI,NC,54', '', ( #19582 ) ) ;
#13037=ORIENTED_EDGE ( 'NONE', *, *, #15864, .F. ) ;
#13058=DIRECTION ( 'NONE',  ( 0.000000000000000000, 0.000000000000000000, -1.000000000000000000 ) ) ;
#13060=EDGE_CURVE ( 'NONE', #8089, #16217, #19276, .T. ) ;
#13068=EDGE_CURVE ( 'NONE', #13441, #7892, #15034, .T. ) ;
#13080=ORIENTED_EDGE ( 'NONE', *, *, #13855, .T. ) ;
#13095=DIRECTION ( 'NONE',  ( 1.000000000000000000, 0.000000000000000000, 0.000000000000000000 ) ) ;
#13113=CARTESIAN_POINT ( 'NONE',  ( -10.00000000000000888, 0.000000000000000000, -103.6250000000000284 ) ) ;
#13167=CARTESIAN_POINT ( 'NONE',  ( 7.395799999999999486, 0.000000000000000000, 0.000000000000000000 ) ) ;
#13176=CARTESIAN_POINT ( 'NONE',  ( 7.999999999999979572, 0.000000000000000000, 0.000000000000000000 ) ) ;
#13224=CARTESIAN_POINT ( 'NONE',  ( -8.000000000000007105, 0.000000000000000000, 0.000000000000000000 ) ) ;
#13227=CIRCLE ( 'NONE', #1942, 101.1000000000000369 ) ;
#13229=VECTOR ( 'NONE', #14974, 1000.000000000000000 ) ;
#13253=CARTESIAN_POINT ( 'NONE',  ( 8.899999999999991473, 0.000000000000000000, -120.0000000000000568 ) ) ;
#13286=EDGE_CURVE ( 'NONE', #19526, #3248, #1292, .T. ) ;
#13298=PLANE ( 'NONE',  #1045 ) ;
#13325=AXIS2_PLACEMENT_3D ( 'NONE', #9007, #3509, #624 ) ;
#13336=DIRECTION ( 'NONE',  ( -1.000000000000000000, 0.000000000000000000, 0.000000000000000000 ) ) ;
#13360=ORIENTED_EDGE ( 'NONE', *, *, #13801, .T. ) ;
#13374=ORIENTED_EDGE ( 'NONE', *, *, #18368, .T. ) ;
#13386=EDGE_LOOP ( 'NONE', ( #9489, #21529 ) ) ;
#13397=ADVANCED_FACE ( 'NONE', ( #20793 ), #10817, .T. ) ;
#13417=EDGE_LOOP ( 'NONE', ( #20105, #19996, #12108, #9791 ) ) ;
#13425=DIRECTION ( 'NONE',  ( 0.000000000000000000, 1.000000000000000000, -1.224646799147353207E-16 ) ) ;
#13441=VERTEX_POINT ( 'NONE', #2334 ) ;
#13451=DIRECTION ( 'NONE',  ( 0.000000000000000000, 0.000000000000000000, -1.000000000000000000 ) ) ;
#13481=CIRCLE ( 'NONE', #14193, 0.2042000000000016025 ) ;
#13511=ORIENTED_EDGE ( 'NONE', *, *, #12177, .T. ) ;
#13514=( NAMED_UNIT ( * ) PLANE_ANGLE_UNIT ( ) SI_UNIT ( $, .RADIAN. ) );
#13515=ORIENTED_EDGE ( 'NONE', *, *, #3537, .T. ) ;
#13516=AXIS2_PLACEMENT_3D ( 'NONE', #492, #2360, #19268 ) ;
#13527=CARTESIAN_POINT ( 'NONE',  ( -90.00000000000000000, 0.000000000000000000, 0.000000000000000000 ) ) ;
#13569=AXIS2_PLACEMENT_3D ( 'NONE', #13527, #8667, #11663 ) ;
#13571=SURFACE_STYLE_USAGE ( .BOTH. , #8391 ) ;
#13594=CIRCLE ( 'NONE', #7591, 118.9000000000000199 ) ;
#13614=CIRCLE ( 'NONE', #9364, 115.1000000000000227 ) ;
#13620=ADVANCED_FACE ( 'NONE', ( #10163 ), #3316, .F. ) ;
#13628=AXIS2_PLACEMENT_3D ( 'NONE', #15371, #15489, #18484 ) ;
#13673=EDGE_CURVE ( 'NONE', #7456, #19336, #17129, .T. ) ;
#13678=FACE_OUTER_BOUND ( 'NONE', #12697, .T. ) ;
#13684=CARTESIAN_POINT ( 'NONE',  ( 7.440711023145602176, 0.000000000000000000, 0.000000000000000000 ) ) ;
#13718=ORIENTED_EDGE ( 'NONE', *, *, #11441, .F. ) ;
#13749=ORIENTED_EDGE ( 'NONE', *, *, #6514, .T. ) ;
#13753=CARTESIAN_POINT ( 'NONE',  ( 8.000000000000007105, 1.284654492305574008E-14, 104.9000000000000341 ) ) ;
#13756=CYLINDRICAL_SURFACE ( 'NONE', #11804, 104.9000000000000341 ) ;
#13776=DIRECTION ( 'NONE',  ( 1.000000000000000000, 0.000000000000000000, 0.000000000000000000 ) ) ;
#13779=DIRECTION ( 'NONE',  ( 1.000000000000000000, 0.000000000000000000, 0.000000000000000000 ) ) ;
#13795=SURFACE_STYLE_FILL_AREA ( #1647 ) ;
#13801=EDGE_CURVE ( 'NONE', #9924, #15910, #1667, .T. ) ;
#13813=CARTESIAN_POINT ( 'NONE',  ( -8.000000000000007105, 0.000000000000000000, 0.000000000000000000 ) ) ;
#13818=AXIS2_PLACEMENT_3D ( 'NONE', #8985, #3810, #10542 ) ;
#13855=EDGE_CURVE ( 'NONE', #16620, #6035, #2009, .T. ) ;
#13887=DIRECTION ( 'NONE',  ( 0.000000000000000000, 0.000000000000000000, -1.000000000000000000 ) ) ;
#13901=CARTESIAN_POINT ( 'NONE',  ( -90.00000000000000000, 0.000000000000000000, 0.000000000000000000 ) ) ;
#13902=LINE ( 'NONE', #19914, #19220 ) ;
#13926=AXIS2_PLACEMENT_3D ( 'NONE', #4962, #7945, #21422 ) ;
#13940=DIRECTION ( 'NONE',  ( 0.000000000000000000, 0.000000000000000000, -1.000000000000000000 ) ) ;
#13957=EDGE_LOOP ( 'NONE', ( #1436, #18879, #12795, #12803 ) ) ;
#13970=CARTESIAN_POINT ( 'NONE',  ( 7.999999999999979572, 0.000000000000000000, 0.000000000000000000 ) ) ;
#13999=DIRECTION ( 'NONE',  ( 1.000000000000000000, -0.000000000000000000, -0.000000000000000000 ) ) ;
#14001=ORIENTED_EDGE ( 'NONE', *, *, #16516, .F. ) ;
#14007=AXIS2_PLACEMENT_3D ( 'NONE', #14235, #3967, #15998 ) ;
#14015=DIRECTION ( 'NONE',  ( 1.000000000000000000, 0.000000000000000000, 0.000000000000000000 ) ) ;
#14044=AXIS2_PLACEMENT_3D ( 'NONE', #20572, #5439, #3776 ) ;
#14098=VERTEX_POINT ( 'NONE', #3612 ) ;
#14110=CARTESIAN_POINT ( 'NONE',  ( 7.599999999999998757, 1.408348717606652665E-14, 114.9007999999999896 ) ) ;
#14167=CYLINDRICAL_SURFACE ( 'NONE', #6525, 100.0000000000000284 ) ;
#14193=AXIS2_PLACEMENT_3D ( 'NONE', #11607, #8401, #11932 ) ;
#14198=TOROIDAL_SURFACE ( 'NONE', #20564, 105.0992000000000104, 0.2041999999999998816 ) ;
#14199=ORIENTED_EDGE ( 'NONE', *, *, #2710, .F. ) ;
#14215=DIRECTION ( 'NONE',  ( 1.000000000000000000, 0.000000000000000000, 0.000000000000000000 ) ) ;
#14219=EDGE_LOOP ( 'NONE', ( #16459, #9082, #17551, #21430 ) ) ;
#14226=DIRECTION ( 'NONE',  ( 0.000000000000000000, 0.000000000000000000, -1.000000000000000000 ) ) ;
#14235=CARTESIAN_POINT ( 'NONE',  ( 8.000000000000007105, 0.000000000000000000, 0.000000000000000000 ) ) ;
#14236=DIRECTION ( 'NONE',  ( 0.000000000000000000, 0.000000000000000000, -1.000000000000000000 ) ) ;
#14242=EDGE_LOOP ( 'NONE', ( #19117, #5431, #11831, #4803 ) ) ;
#14243=EDGE_LOOP ( 'NONE', ( #9221, #3826, #1273, #14001 ) ) ;
#14244=AXIS2_PLACEMENT_3D ( 'NONE', #3041, #11104, #9543 ) ;
#14286=DIRECTION ( 'NONE',  ( 0.000000000000000000, 0.000000000000000000, -1.000000000000000000 ) ) ;
#14345=FACE_OUTER_BOUND ( 'NONE', #967, .T. ) ;
#14350=CARTESIAN_POINT ( 'NONE',  ( -8.000000000000007105, 1.409568465818603827E-14, 115.1000000000000227 ) ) ;
#14369=AXIS2_PLACEMENT_3D ( 'NONE', #15884, #9556, #11007 ) ;
#14370=CARTESIAN_POINT ( 'NONE',  ( -8.000000000000007105, 0.000000000000000000, 0.000000000000000000 ) ) ;
#14398=CARTESIAN_POINT ( 'NONE',  ( 9.999999999999994671, 0.000000000000000000, 103.6249999999999716 ) ) ;
#14411=AXIS2_PLACEMENT_3D ( 'NONE', #11176, #2889, #5190 ) ;
#14415=CIRCLE ( 'NONE', #11602, 101.1000000000000512 ) ;
#14421=ORIENTED_EDGE ( 'NONE', *, *, #9403, .T. ) ;
#14433=COLOUR_RGB ( '', 0.08235294, 0.09019608, 0.10196078) ;
#14444=ORIENTED_EDGE ( 'NONE', *, *, #17340, .F. ) ;
#14474=ORIENTED_EDGE ( 'NONE', *, *, #14843, .F. ) ;
#14509=CARTESIAN_POINT ( 'NONE',  ( 7.440711023145602176, 0.000000000000000000, -115.1000000000000227 ) ) ;
#14522=( GEOMETRIC_REPRESENTATION_CONTEXT ( 3 ) GLOBAL_UNCERTAINTY_ASSIGNED_CONTEXT ( ( #4818 ) ) GLOBAL_UNIT_ASSIGNED_CONTEXT ( ( #2589, #4476, #8220 ) ) REPRESENTATION_CONTEXT ( 'NONE', 'WORKASPACE' ) );
#14536=DIRECTION ( 'NONE',  ( 1.000000000000000000, 0.000000000000000000, 0.000000000000000000 ) ) ;
#14538=PRODUCT_DEFINITION_FORMATION_WITH_SPECIFIED_SOURCE ( 'ANY', '', #13018, .NOT_KNOWN. ) ;
#14583=DIRECTION ( 'NONE',  ( -1.000000000000000000, -0.000000000000000000, -0.000000000000000000 ) ) ;
#14628=CARTESIAN_POINT ( 'NONE',  ( -10.00000000000002309, 0.000000000000000000, 0.000000000000000000 ) ) ;
#14637=CIRCLE ( 'NONE', #867, 113.8250000000000028 ) ;
#14644=FACE_BOUND ( 'NONE', #11294, .T. ) ;
#14645=CARTESIAN_POINT ( 'NONE',  ( -7.395799999999999486, 1.407128969394701661E-14, 114.9007999999999896 ) ) ;
#14653=AXIS2_PLACEMENT_3D ( 'NONE', #20744, #7153, #13887 ) ;
#14661=ORIENTED_EDGE ( 'NONE', *, *, #8157, .F. ) ;
#14685=AXIS2_PLACEMENT_3D ( 'NONE', #11081, #12842, #15943 ) ;
#14768=DIRECTION ( 'NONE',  ( 0.000000000000000000, 0.000000000000000000, -1.000000000000000000 ) ) ;
#14830=ORIENTED_EDGE ( 'NONE', *, *, #16507, .T. ) ;
#14841=VECTOR ( 'NONE', #2735, 1000.000000000000000 ) ;
#14843=EDGE_CURVE ( 'NONE', #18019, #8212, #17238, .T. ) ;
#14851=ORIENTED_EDGE ( 'NONE', *, *, #8255, .T. ) ;
#14876=CARTESIAN_POINT ( 'NONE',  ( 7.440711023145912151, 0.000000000000000000, -104.9000000000000341 ) ) ;
#14974=DIRECTION ( 'NONE',  ( 1.000000000000000000, 0.000000000000000000, 0.000000000000000000 ) ) ;
#14977=EDGE_LOOP ( 'NONE', ( #19602, #13511, #16998, #18994 ) ) ;
#14993=ORIENTED_EDGE ( 'NONE', *, *, #15533, .T. ) ;
#15011=EDGE_CURVE ( 'NONE', #19408, #20730, #10899, .T. ) ;
#15030=DIRECTION ( 'NONE',  ( 0.000000000000000000, 0.000000000000000000, -1.000000000000000000 ) ) ;
#15034=CIRCLE ( 'NONE', #14685, 101.1000000000000369 ) ;
#15064=ORIENTED_EDGE ( 'NONE', *, *, #13286, .T. ) ;
#15075=CARTESIAN_POINT ( 'NONE',  ( -90.00000000000000000, 1.409568465818603827E-14, 115.1000000000000227 ) ) ;
#15116=( LENGTH_UNIT ( ) NAMED_UNIT ( * ) SI_UNIT ( .MILLI., .METRE. ) );
#15119=ORIENTED_EDGE ( 'NONE', *, *, #1093, .T. ) ;
#15141=CIRCLE ( 'NONE', #20795, 0.2042000000000016025 ) ;
#15143=ORIENTED_EDGE ( 'NONE', *, *, #2343, .T. ) ;
#15203=EDGE_LOOP ( 'NONE', ( #1171, #16549, #18916, #21380 ) ) ;
#15206=CARTESIAN_POINT ( 'NONE',  ( -7.600000000000002309, 0.000000000000000000, -114.9007999999999896 ) ) ;
#15209=DIRECTION ( 'NONE',  ( 0.000000000000000000, 0.000000000000000000, -1.000000000000000000 ) ) ;
#15210=DIRECTION ( 'NONE',  ( 1.000000000000000000, 0.000000000000000000, 0.000000000000000000 ) ) ;
#15338=AXIS2_PLACEMENT_3D ( 'NONE', #19213, #9153, #15900 ) ;
#15346=DIRECTION ( 'NONE',  ( 1.000000000000000000, 0.000000000000000000, 0.000000000000000000 ) ) ;
#15366=ORIENTED_EDGE ( 'NONE', *, *, #13286, .F. ) ;
#15367=CARTESIAN_POINT ( 'NONE',  ( 9.999999999999980460, 0.000000000000000000, -113.8250000000000171 ) ) ;
#15371=CARTESIAN_POINT ( 'NONE',  ( 7.599999999999998757, 0.000000000000000000, 0.000000000000000000 ) ) ;
#15387=SURFACE_SIDE_STYLE ('',( #18400 ) ) ;
#15388=AXIS2_PLACEMENT_3D ( 'NONE', #18756, #20523, #17213 ) ;
#15426=DIRECTION ( 'NONE',  ( 1.000000000000000000, -0.000000000000000000, -0.000000000000000000 ) ) ;
#15432=FACE_OUTER_BOUND ( 'NONE', #4613, .T. ) ;
#15466=DIRECTION ( 'NONE',  ( 0.000000000000000000, 0.000000000000000000, -1.000000000000000000 ) ) ;
#15487=DIRECTION ( 'NONE',  ( 1.000000000000000000, 0.000000000000000000, 0.000000000000000000 ) ) ;
#15489=DIRECTION ( 'NONE',  ( 1.000000000000000000, -0.000000000000000000, -0.000000000000000000 ) ) ;
#15511=VERTEX_POINT ( 'NONE', #14110 ) ;
#15533=EDGE_CURVE ( 'NONE', #3248, #18016, #15141, .T. ) ;
#15567=AXIS2_PLACEMENT_3D ( 'NONE', #21837, #20187, #17085 ) ;
#15573=DIRECTION ( 'NONE',  ( 0.000000000000000000, 0.000000000000000000, -1.000000000000000000 ) ) ;
#15581=ORIENTED_EDGE ( 'NONE', *, *, #5698, .F. ) ;
#15623=ADVANCED_FACE ( 'NONE', ( #18080, #7697 ), #1406, .T. ) ;
#15637=ORIENTED_EDGE ( 'NONE', *, *, #16228, .T. ) ;
#15641=LINE ( 'NONE', #512, #9311 ) ;
#15656=EDGE_CURVE ( 'NONE', #993, #19336, #1419, .T. ) ;
#15663=VERTEX_POINT ( 'NONE', #21513 ) ;
#15682=ORIENTED_EDGE ( 'NONE', *, *, #8255, .F. ) ;
#15701=AXIS2_PLACEMENT_3D ( 'NONE', #16600, #18778, #3859 ) ;
#15758=PLANE ( 'NONE',  #13325 ) ;
#15769=AXIS2_PLACEMENT_3D ( 'NONE', #8839, #1991, #15573 ) ;
#15800=LINE ( 'NONE', #18092, #14841 ) ;
#15815=CIRCLE ( 'NONE', #14044, 1.100000000000003642 ) ;
#15831=DIRECTION ( 'NONE',  ( 1.000000000000000000, 0.000000000000000000, 0.000000000000000000 ) ) ;
#15849=DIRECTION ( 'NONE',  ( -0.000000000000000000, -1.000000000000000000, -0.000000000000000000 ) ) ;
#15864=EDGE_CURVE ( 'NONE', #10257, #12527, #12411, .T. ) ;
#15866=ORIENTED_EDGE ( 'NONE', *, *, #16707, .F. ) ;
#15884=CARTESIAN_POINT ( 'NONE',  ( 7.599999999999998757, 105.0992000000000104, 0.000000000000000000 ) ) ;
#15888=CIRCLE ( 'NONE', #11291, 1.100000000000017630 ) ;
#15900=DIRECTION ( 'NONE',  ( 0.000000000000000000, 0.000000000000000000, -1.000000000000000000 ) ) ;
#15904=CARTESIAN_POINT ( 'NONE',  ( 9.999999999999994671, 1.276847368961009200E-14, -103.6249999999999716 ) ) ;
#15910=VERTEX_POINT ( 'NONE', #8786 ) ;
#15917=DIRECTION ( 'NONE',  ( 0.000000000000000000, 0.000000000000000000, -1.000000000000000000 ) ) ;
#15918=CARTESIAN_POINT ( 'NONE',  ( 7.599999999999998757, 0.000000000000000000, 0.000000000000000000 ) ) ;
#15925=DIRECTION ( 'NONE',  ( 0.000000000000000000, 0.000000000000000000, -1.000000000000000000 ) ) ;
#15943=DIRECTION ( 'NONE',  ( 0.000000000000000000, 0.000000000000000000, -1.000000000000000000 ) ) ;
#15945=CARTESIAN_POINT ( 'NONE',  ( 7.395800000000001262, 0.000000000000000000, -114.9007999999999896 ) ) ;
#15966=DIRECTION ( 'NONE',  ( 0.000000000000000000, 0.000000000000000000, -1.000000000000000000 ) ) ;
#15977=CARTESIAN_POINT ( 'NONE',  ( -8.000000000000007105, 1.393954219129474843E-14, 113.8250000000000028 ) ) ;
#15998=DIRECTION ( 'NONE',  ( 0.000000000000000000, 0.000000000000000000, -1.000000000000000000 ) ) ;
#16030=CIRCLE ( 'NONE', #19924, 118.9000000000000199 ) ;
#16093=DIRECTION ( 'NONE',  ( 0.000000000000000000, 0.000000000000000000, -1.000000000000000000 ) ) ;
#16110=CARTESIAN_POINT ( 'NONE',  ( 7.999999999999979572, 0.000000000000000000, -113.8250000000000171 ) ) ;
#16140=DIRECTION ( 'NONE',  ( 1.000000000000000000, -0.000000000000000000, -0.000000000000000000 ) ) ;
#16184=AXIS2_PLACEMENT_3D ( 'NONE', #19413, #12769, #6167 ) ;
#16185=DIRECTION ( 'NONE',  ( 1.000000000000000000, 0.000000000000000000, 0.000000000000000000 ) ) ;
#16187=ORIENTED_EDGE ( 'NONE', *, *, #12306, .T. ) ;
#16217=VERTEX_POINT ( 'NONE', #884 ) ;
#16227=CARTESIAN_POINT ( 'NONE',  ( -8.900000000000019895, 0.000000000000000000, -100.0000000000000284 ) ) ;
#16228=EDGE_CURVE ( 'NONE', #6035, #16620, #14637, .T. ) ;
#16247=EDGE_CURVE ( 'NONE', #5584, #5601, #4403, .T. ) ;
#16255=EDGE_CURVE ( 'NONE', #1245, #2769, #16030, .T. ) ;
#16290=DIRECTION ( 'NONE',  ( 1.000000000000000000, -0.000000000000000000, -0.000000000000000000 ) ) ;
#16370=ADVANCED_FACE ( 'NONE', ( #13678 ), #1944, .T. ) ;
#16394=DIRECTION ( 'NONE',  ( 1.000000000000000000, 0.000000000000000000, 0.000000000000000000 ) ) ;
#16403=CARTESIAN_POINT ( 'NONE',  ( -8.000000000000007105, 0.000000000000000000, 0.000000000000000000 ) ) ;
#16445=SHAPE_REPRESENTATION ( 'radial cylindrical roller bearing_iso_ISO 15 RCR - 17200 - 54,SI,NC,54', ( #15567 ), #14522 ) ;
#16459=ORIENTED_EDGE ( 'NONE', *, *, #5969, .F. ) ;
#16507=EDGE_CURVE ( 'NONE', #15910, #9924, #18889, .T. ) ;
#16516=EDGE_CURVE ( 'NONE', #2769, #1245, #13594, .T. ) ;
#16549=ORIENTED_EDGE ( 'NONE', *, *, #12983, .T. ) ;
#16558=TOROIDAL_SURFACE ( 'NONE', #21147, 101.1000000000000512, 1.100000000000009859 ) ;
#16571=VECTOR ( 'NONE', #10330, 1000.000000000000000 ) ;
#16600=CARTESIAN_POINT ( 'NONE',  ( 8.899999999999987921, 0.000000000000000000, 0.000000000000000000 ) ) ;
#16620=VERTEX_POINT ( 'NONE', #15977 ) ;
#16631=ADVANCED_FACE ( 'NONE', ( #19633 ), #10057, .T. ) ;
#16642=ORIENTED_EDGE ( 'NONE', *, *, #7828, .T. ) ;
#16651=CARTESIAN_POINT ( 'NONE',  ( -90.00000000000000000, 1.284654492305574008E-14, 104.9000000000000341 ) ) ;
#16707=EDGE_CURVE ( 'NONE', #18401, #993, #2938, .T. ) ;
#16712=EDGE_LOOP ( 'NONE', ( #10170, #17352, #5276, #18288 ) ) ;
#16715=APPLICATION_CONTEXT ( 'automotive_design' ) ;
#16761=AXIS2_PLACEMENT_3D ( 'NONE', #9147, #19529, #7497 ) ;
#16781=FILL_AREA_STYLE_COLOUR ( '', #14433 ) ;
#16800=DIRECTION ( 'NONE',  ( 1.000000000000000000, 0.000000000000000000, 0.000000000000000000 ) ) ;
#16830=AXIS2_PLACEMENT_3D ( 'NONE', #13813, #17017, #345 ) ;
#16857=ADVANCED_FACE ( 'NONE', ( #9179 ), #5037, .T. ) ;
#16879=CARTESIAN_POINT ( 'NONE',  ( -8.000000000000007105, 0.000000000000000000, 0.000000000000000000 ) ) ;
#16941=DIRECTION ( 'NONE',  ( 0.000000000000000000, 0.000000000000000000, -1.000000000000000000 ) ) ;
#16987=CYLINDRICAL_SURFACE ( 'NONE', #11215, 104.9000000000000341 ) ;
#16998=ORIENTED_EDGE ( 'NONE', *, *, #1796, .T. ) ;
#16999=PRESENTATION_STYLE_ASSIGNMENT (( #13571 ) ) ;
#17017=DIRECTION ( 'NONE',  ( 1.000000000000000000, 0.000000000000000000, 0.000000000000000000 ) ) ;
#17019=VERTEX_POINT ( 'NONE', #19792 ) ;
#17024=ORIENTED_EDGE ( 'NONE', *, *, #20558, .F. ) ;
#17085=DIRECTION ( 'NONE',  ( 1.000000000000000000, 0.000000000000000000, 0.000000000000000000 ) ) ;
#17088=ORIENTED_EDGE ( 'NONE', *, *, #6366, .F. ) ;
#17110=DIRECTION ( 'NONE',  ( 0.000000000000000000, 0.000000000000000000, 1.000000000000000000 ) ) ;
#17124=CARTESIAN_POINT ( 'NONE',  ( -8.000000000000007105, 0.000000000000000000, -113.8250000000000028 ) ) ;
#17129=LINE ( 'NONE', #12143, #2366 ) ;
#17153=AXIS2_PLACEMENT_3D ( 'NONE', #2342, #10325, #15925 ) ;
#17158=CYLINDRICAL_SURFACE ( 'NONE', #10565, 100.0000000000000284 ) ;
#17189=ORIENTED_EDGE ( 'NONE', *, *, #16255, .F. ) ;
#17213=DIRECTION ( 'NONE',  ( 0.000000000000000000, 0.000000000000000000, -1.000000000000000000 ) ) ;
#17233=CIRCLE ( 'NONE', #2054, 120.0000000000000568 ) ;
#17237=VECTOR ( 'NONE', #15831, 1000.000000000000000 ) ;
#17238=CIRCLE ( 'NONE', #17253, 114.9007999999999896 ) ;
#17253=AXIS2_PLACEMENT_3D ( 'NONE', #21330, #21443, #15030 ) ;
#17270=DIRECTION ( 'NONE',  ( 0.000000000000000000, 1.224646799147322392E-16, 1.000000000000000000 ) ) ;
#17296=FACE_OUTER_BOUND ( 'NONE', #10406, .T. ) ;
#17340=EDGE_CURVE ( 'NONE', #1609, #9924, #2111, .T. ) ;
#17342=DIRECTION ( 'NONE',  ( 0.000000000000000000, 0.000000000000000000, -1.000000000000000000 ) ) ;
#17352=ORIENTED_EDGE ( 'NONE', *, *, #20341, .F. ) ;
#17376=CARTESIAN_POINT ( 'NONE',  ( -7.600000000000002309, 0.000000000000000000, 0.000000000000000000 ) ) ;
#17393=DIRECTION ( 'NONE',  ( 0.000000000000000000, 0.000000000000000000, -1.000000000000000000 ) ) ;
#17400=DIRECTION ( 'NONE',  ( 1.000000000000000000, 0.000000000000000000, 0.000000000000000000 ) ) ;
#17408=DIRECTION ( 'NONE',  ( 0.000000000000000000, 0.000000000000000000, -1.000000000000000000 ) ) ;
#17412=VERTEX_POINT ( 'NONE', #15904 ) ;
#17421=DIRECTION ( 'NONE',  ( 1.000000000000000000, 0.000000000000000000, 0.000000000000000000 ) ) ;
#17428=DIRECTION ( 'NONE',  ( 0.000000000000000000, 0.000000000000000000, -1.000000000000000000 ) ) ;
#17432=AXIS2_PLACEMENT_3D ( 'NONE', #626, #12656, #2603 ) ;
#17436=ADVANCED_FACE ( 'NONE', ( #18014, #12695 ), #21208, .T. ) ;
#17457=CARTESIAN_POINT ( 'NONE',  ( 7.395799999999999486, 1.287093988729475069E-14, 105.0992000000000104 ) ) ;
#17461=ORIENTED_EDGE ( 'NONE', *, *, #445, .T. ) ;
#17475=CIRCLE ( 'NONE', #20301, 118.9000000000000199 ) ;
#17476=DIRECTION ( 'NONE',  ( 0.000000000000000000, 1.000000000000000000, -1.224646799147353207E-16 ) ) ;
#17513=DIRECTION ( 'NONE',  ( 0.000000000000000000, 0.000000000000000000, -1.000000000000000000 ) ) ;
#17520=CARTESIAN_POINT ( 'NONE',  ( -8.900000000000012790, 0.000000000000000000, 0.000000000000000000 ) ) ;
#17538=CYLINDRICAL_SURFACE ( 'NONE', #15388, 113.8250000000000028 ) ;
#17551=ORIENTED_EDGE ( 'NONE', *, *, #2788, .T. ) ;
#17587=DIRECTION ( 'NONE',  ( 1.000000000000000000, 0.000000000000000000, 0.000000000000000000 ) ) ;
#17654=DIRECTION ( 'NONE',  ( -0.8432271980573100567, 6.583178742725224615E-17, -0.5375573387615669718 ) ) ;
#17663=ORIENTED_EDGE ( 'NONE', *, *, #4323, .T. ) ;
#17685=ORIENTED_EDGE ( 'NONE', *, *, #15656, .F. ) ;
#17720=DIRECTION ( 'NONE',  ( 0.000000000000000000, 0.000000000000000000, -1.000000000000000000 ) ) ;
#17733=DIRECTION ( 'NONE',  ( 1.000000000000000000, 0.000000000000000000, 0.000000000000000000 ) ) ;
#17736=LINE ( 'NONE', #2586, #8808 ) ;
#17837=EDGE_CURVE ( 'NONE', #17412, #15910, #7593, .T. ) ;
#17839=ADVANCED_FACE ( 'NONE', ( #21183, #9133 ), #6164, .T. ) ;
#17854=ORIENTED_EDGE ( 'NONE', *, *, #20341, .T. ) ;
#17873=DIRECTION ( 'NONE',  ( 0.000000000000000000, 0.000000000000000000, -1.000000000000000000 ) ) ;
#17960=CIRCLE ( 'NONE', #4915, 115.1000000000000227 ) ;
#18014=FACE_OUTER_BOUND ( 'NONE', #1540, .T. ) ;
#18016=VERTEX_POINT ( 'NONE', #14876 ) ;
#18019=VERTEX_POINT ( 'NONE', #20182 ) ;
#18024=ORIENTED_EDGE ( 'NONE', *, *, #9290, .F. ) ;
#18027=CARTESIAN_POINT ( 'NONE',  ( -8.900000000000019895, 0.000000000000000000, 0.000000000000000000 ) ) ;
#18048=DIRECTION ( 'NONE',  ( 1.000000000000000000, 0.000000000000000000, 0.000000000000000000 ) ) ;
#18071=CIRCLE ( 'NONE', #20882, 104.9000000000000341 ) ;
#18077=CARTESIAN_POINT ( 'NONE',  ( -7.395799999999999486, 0.000000000000000000, -114.9007999999999896 ) ) ;
#18080=FACE_BOUND ( 'NONE', #7339, .T. ) ;
#18092=CARTESIAN_POINT ( 'NONE',  ( -90.00000000000000000, 0.000000000000000000, -104.9000000000000341 ) ) ;
#18110=CARTESIAN_POINT ( 'NONE',  ( 10.00000000000000888, 0.000000000000000000, 0.000000000000000000 ) ) ;
#18119=AXIS2_PLACEMENT_3D ( 'NONE', #5149, #5681, #19056 ) ;
#18137=ORIENTED_EDGE ( 'NONE', *, *, #9594, .T. ) ;
#18153=DIRECTION ( 'NONE',  ( 1.000000000000000000, 0.000000000000000000, 0.000000000000000000 ) ) ;
#18175=FACE_OUTER_BOUND ( 'NONE', #6360, .T. ) ;
#18197=DIRECTION ( 'NONE',  ( -1.000000000000000000, 0.000000000000000000, -0.000000000000000000 ) ) ;
#18215=LINE ( 'NONE', #13013, #20988 ) ;
#18257=ADVANCED_FACE ( 'NONE', ( #10760 ), #4151, .T. ) ;
#18274=DIRECTION ( 'NONE',  ( 1.000000000000000000, -0.000000000000000000, -0.000000000000000000 ) ) ;
#18285=AXIS2_PLACEMENT_3D ( 'NONE', #6993, #18713, #12060 ) ;
#18288=ORIENTED_EDGE ( 'NONE', *, *, #12818, .T. ) ;
#18300=DIRECTION ( 'NONE',  ( 0.000000000000000000, 0.000000000000000000, -1.000000000000000000 ) ) ;
#18335=DIRECTION ( 'NONE',  ( 0.000000000000000000, 0.000000000000000000, 1.000000000000000000 ) ) ;
#18368=EDGE_CURVE ( 'NONE', #17019, #12527, #10141, .T. ) ;
#18400=SURFACE_STYLE_FILL_AREA ( #154 ) ;
#18401=VERTEX_POINT ( 'NONE', #12968 ) ;
#18408=EDGE_CURVE ( 'NONE', #1529, #19408, #10862, .T. ) ;
#18420=CARTESIAN_POINT ( 'NONE',  ( -90.00000000000000000, 0.000000000000000000, -115.1000000000000227 ) ) ;
#18421=ORIENTED_EDGE ( 'NONE', *, *, #9290, .T. ) ;
#18438=FACE_OUTER_BOUND ( 'NONE', #11493, .T. ) ;
#18467=AXIS2_PLACEMENT_3D ( 'NONE', #10921, #5962, #7612 ) ;
#18474=FACE_OUTER_BOUND ( 'NONE', #1981, .T. ) ;
#18484=DIRECTION ( 'NONE',  ( 0.000000000000000000, 0.000000000000000000, -1.000000000000000000 ) ) ;
#18496=ORIENTED_EDGE ( 'NONE', *, *, #3650, .T. ) ;
#18502=DIRECTION ( 'NONE',  ( 1.000000000000000000, 0.000000000000000000, 0.000000000000000000 ) ) ;
#18558=( NAMED_UNIT ( * ) SI_UNIT ( $, .STERADIAN. ) SOLID_ANGLE_UNIT ( ) );
#18570=ORIENTED_EDGE ( 'NONE', *, *, #11328, .F. ) ;
#18609=EDGE_CURVE ( 'NONE', #18016, #15910, #2344, .T. ) ;
#18612=FILL_AREA_STYLE_COLOUR ( '', #4286 ) ;
#18631=ORIENTED_EDGE ( 'NONE', *, *, #5662, .T. ) ;
#18713=DIRECTION ( 'NONE',  ( 1.000000000000000000, 0.000000000000000000, 0.000000000000000000 ) ) ;
#18756=CARTESIAN_POINT ( 'NONE',  ( -90.00000000000000000, 0.000000000000000000, 0.000000000000000000 ) ) ;
#18757=VECTOR ( 'NONE', #20500, 1000.000000000000227 ) ;
#18764=CARTESIAN_POINT ( 'NONE',  ( -7.395799999999999486, 0.000000000000000000, 0.000000000000000000 ) ) ;
#18778=DIRECTION ( 'NONE',  ( 1.000000000000000000, 0.000000000000000000, 0.000000000000000000 ) ) ;
#18795=ADVANCED_FACE ( 'NONE', ( #6849, #10148 ), #1651, .T. ) ;
#18801=DIRECTION ( 'NONE',  ( 0.000000000000000000, 1.224646799147354933E-16, 1.000000000000000000 ) ) ;
#18805=AXIS2_PLACEMENT_3D ( 'NONE', #434, #7081, #340 ) ;
#18825=ORIENTED_EDGE ( 'NONE', *, *, #6514, .F. ) ;
#18835=CIRCLE ( 'NONE', #486, 104.9000000000000341 ) ;
#18847=CONICAL_SURFACE ( 'NONE', #840, 104.9000000000000341, 0.5675376247847546685 ) ;
#18851=CARTESIAN_POINT ( 'NONE',  ( 7.440711023145602176, 1.409568465818603827E-14, 115.1000000000000227 ) ) ;
#18863=DIRECTION ( 'NONE',  ( 1.000000000000000000, 0.000000000000000000, 0.000000000000000000 ) ) ;
#18878=DIRECTION ( 'NONE',  ( 0.000000000000000000, 0.000000000000000000, -1.000000000000000000 ) ) ;
#18879=ORIENTED_EDGE ( 'NONE', *, *, #856, .F. ) ;
#18889=CIRCLE ( 'NONE', #14653, 104.9000000000000341 ) ;
#18916=ORIENTED_EDGE ( 'NONE', *, *, #2761, .T. ) ;
#18962=DIRECTION ( 'NONE',  ( 1.000000000000000000, 0.000000000000000000, 0.000000000000000000 ) ) ;
#18994=ORIENTED_EDGE ( 'NONE', *, *, #21717, .F. ) ;
#18996=DIRECTION ( 'NONE',  ( 1.000000000000000000, 0.000000000000000000, 0.000000000000000000 ) ) ;
#19056=DIRECTION ( 'NONE',  ( 0.000000000000000000, 0.000000000000000000, -1.000000000000000000 ) ) ;
#19075=AXIS2_PLACEMENT_3D ( 'NONE', #10521, #8862, #12938 ) ;
#19080=CARTESIAN_POINT ( 'NONE',  ( -90.00000000000000000, 0.000000000000000000, 0.000000000000000000 ) ) ;
#19117=ORIENTED_EDGE ( 'NONE', *, *, #18408, .T. ) ;
#19213=CARTESIAN_POINT ( 'NONE',  ( -7.600000000000002309, 0.000000000000000000, 0.000000000000000000 ) ) ;
#19214=DIRECTION ( 'NONE',  ( 0.000000000000000000, 1.000000000000000000, -1.224646799147353207E-16 ) ) ;
#19220=VECTOR ( 'NONE', #3632, 1000.000000000000000 ) ;
#19236=CIRCLE ( 'NONE', #4062, 115.1000000000000227 ) ;
#19258=ORIENTED_EDGE ( 'NONE', *, *, #13068, .F. ) ;
#19259=DIRECTION ( 'NONE',  ( 0.000000000000000000, 0.000000000000000000, -1.000000000000000000 ) ) ;
#19268=DIRECTION ( 'NONE',  ( 0.000000000000000000, 0.000000000000000000, -1.000000000000000000 ) ) ;
#19276=CIRCLE ( 'NONE', #7624, 0.2042000000000016025 ) ;
#19292=DIRECTION ( 'NONE',  ( -1.000000000000000000, 0.000000000000000000, 0.000000000000000000 ) ) ;
#19300=DIRECTION ( 'NONE',  ( 1.000000000000000000, 0.000000000000000000, 0.000000000000000000 ) ) ;
#19336=VERTEX_POINT ( 'NONE', #20725 ) ;
#19343=EDGE_CURVE ( 'NONE', #13007, #3216, #8448, .T. ) ;
#19353=CIRCLE ( 'NONE', #10173, 1.100000000000003642 ) ;
#19369=VERTEX_POINT ( 'NONE', #18851 ) ;
#19386=AXIS2_PLACEMENT_3D ( 'NONE', #2700, #2486, #10764 ) ;
#19408=VERTEX_POINT ( 'NONE', #5271 ) ;
#19413=CARTESIAN_POINT ( 'NONE',  ( 7.395799999999999486, 0.000000000000000000, 0.000000000000000000 ) ) ;
#19449=ADVANCED_FACE ( 'NONE', ( #9536 ), #11097, .T. ) ;
#19526=VERTEX_POINT ( 'NONE', #5914 ) ;
#19529=DIRECTION ( 'NONE',  ( 1.000000000000000000, 0.000000000000000000, 0.000000000000000000 ) ) ;
#19545=ORIENTED_EDGE ( 'NONE', *, *, #10560, .T. ) ;
#19566=EDGE_CURVE ( 'NONE', #15663, #9924, #17736, .T. ) ;
#19582=PRODUCT_CONTEXT ( 'NONE', #16715, 'mechanical' ) ;
#19583=DIRECTION ( 'NONE',  ( 1.000000000000000000, 0.000000000000000000, 0.000000000000000000 ) ) ;
#19602=ORIENTED_EDGE ( 'NONE', *, *, #937, .T. ) ;
#19623=ADVANCED_FACE ( 'NONE', ( #19931, #11422 ), #13298, .T. ) ;
#19625=LINE ( 'NONE', #6272, #8079 ) ;
#19632=CONICAL_SURFACE ( 'NONE', #7941, 104.9000000000000341, 0.5675376247847546685 ) ;
#19633=FACE_OUTER_BOUND ( 'NONE', #5446, .T. ) ;
#19636=ORIENTED_EDGE ( 'NONE', *, *, #2485, .F. ) ;
#19638=CARTESIAN_POINT ( 'NONE',  ( 9.999999999999994671, 0.000000000000000000, 0.000000000000000000 ) ) ;
#19643=AXIS2_PLACEMENT_3D ( 'NONE', #6310, #11150, #12791 ) ;
#19645=DIRECTION ( 'NONE',  ( 1.000000000000000000, 0.000000000000000000, 0.000000000000000000 ) ) ;
#19707=CARTESIAN_POINT ( 'NONE',  ( -8.000000000000007105, 0.000000000000000000, -104.9000000000000341 ) ) ;
#19717=MECHANICAL_DESIGN_GEOMETRIC_PRESENTATION_REPRESENTATION('',(#21830),#10193);
#19790=CIRCLE ( 'NONE', #12729, 120.0000000000000284 ) ;
#19792=CARTESIAN_POINT ( 'NONE',  ( 7.999999999999979572, 1.409568465818603827E-14, 115.1000000000000227 ) ) ;
#19825=DIRECTION ( 'NONE',  ( 1.000000000000000000, 0.000000000000000000, 0.000000000000000000 ) ) ;
#19837=CARTESIAN_POINT ( 'NONE',  ( 7.999999999999986677, 113.8250000000000171, 0.000000000000000000 ) ) ;
#19854=ORIENTED_EDGE ( 'NONE', *, *, #20647, .T. ) ;
#19858=TOROIDAL_SURFACE ( 'NONE', #1862, 101.1000000000000369, 1.100000000000002087 ) ;
#19882=DIRECTION ( 'NONE',  ( 0.000000000000000000, 0.000000000000000000, -1.000000000000000000 ) ) ;
#19901=ORIENTED_EDGE ( 'NONE', *, *, #16228, .F. ) ;
#19914=CARTESIAN_POINT ( 'NONE',  ( -90.00000000000000000, 0.000000000000000000, -113.8250000000000171 ) ) ;
#19924=AXIS2_PLACEMENT_3D ( 'NONE', #18110, #21636, #6308 ) ;
#19931=FACE_OUTER_BOUND ( 'NONE', #10328, .T. ) ;
#19975=DIRECTION ( 'NONE',  ( 0.000000000000000000, 0.000000000000000000, -1.000000000000000000 ) ) ;
#19981=AXIS2_PLACEMENT_3D ( 'NONE', #20686, #7427, #17270 ) ;
#19991=ORIENTED_EDGE ( 'NONE', *, *, #8257, .T. ) ;
#19996=ORIENTED_EDGE ( 'NONE', *, *, #3650, .F. ) ;
#20022=DIRECTION ( 'NONE',  ( 0.000000000000000000, 1.000000000000000000, -1.224646799147353207E-16 ) ) ;
#20027=EDGE_LOOP ( 'NONE', ( #1671, #14421, #21145, #6141 ) ) ;
#20040=AXIS2_PLACEMENT_3D ( 'NONE', #17520, #17733, #11205 ) ;
#20091=DIRECTION ( 'NONE',  ( 1.000000000000000000, 0.000000000000000000, 0.000000000000000000 ) ) ;
#20094=DIRECTION ( 'NONE',  ( 1.000000000000000000, -0.000000000000000000, -0.000000000000000000 ) ) ;
#20105=ORIENTED_EDGE ( 'NONE', *, *, #11797, .F. ) ;
#20173=ADVANCED_FACE ( 'NONE', ( #18474 ), #21345, .F. ) ;
#20179=( GEOMETRIC_REPRESENTATION_CONTEXT ( 3 ) GLOBAL_UNCERTAINTY_ASSIGNED_CONTEXT ( ( #9658 ) ) GLOBAL_UNIT_ASSIGNED_CONTEXT ( ( #10091, #13514, #9975 ) ) REPRESENTATION_CONTEXT ( 'NONE', 'WORKASPACE' ) );
#20182=CARTESIAN_POINT ( 'NONE',  ( -7.600000000000002309, 1.408348717606652665E-14, 114.9007999999999896 ) ) ;
#20187=DIRECTION ( 'NONE',  ( 0.000000000000000000, 0.000000000000000000, 1.000000000000000000 ) ) ;
#20197=DIRECTION ( 'NONE',  ( 0.000000000000000000, 0.000000000000000000, -1.000000000000000000 ) ) ;
#20201=CARTESIAN_POINT ( 'NONE',  ( -7.395800000000001262, 0.000000000000000000, 0.000000000000000000 ) ) ;
#20231=CIRCLE ( 'NONE', #13516, 103.6249999999999716 ) ;
#20244=CIRCLE ( 'NONE', #17432, 115.1000000000000227 ) ;
#20253=CYLINDRICAL_SURFACE ( 'NONE', #20984, 115.1000000000000227 ) ;
#20267=PRESENTATION_STYLE_ASSIGNMENT (( #1811 ) ) ;
#20285=ORIENTED_EDGE ( 'NONE', *, *, #1939, .T. ) ;
#20301=AXIS2_PLACEMENT_3D ( 'NONE', #20682, #17587, #5545 ) ;
#20313=DIRECTION ( 'NONE',  ( 1.000000000000000000, -0.000000000000000000, -0.000000000000000000 ) ) ;
#20333=CIRCLE ( 'NONE', #21014, 103.6250000000000284 ) ;
#20339=MANIFOLD_SOLID_BREP ( 'InnerRace', #11137 ) ;
#20341=EDGE_CURVE ( 'NONE', #10257, #19369, #17960, .T. ) ;
#20355=DIRECTION ( 'NONE',  ( 0.000000000000000000, 0.000000000000000000, -1.000000000000000000 ) ) ;
#20372=CIRCLE ( 'NONE', #16830, 104.9000000000000341 ) ;
#20436=DIRECTION ( 'NONE',  ( 1.000000000000000000, -0.000000000000000000, -0.000000000000000000 ) ) ;
#20439=ADVANCED_FACE ( 'NONE', ( #20751 ), #16558, .T. ) ;
#20442=ORIENTED_EDGE ( 'NONE', *, *, #8946, .F. ) ;
#20443=AXIS2_PLACEMENT_3D ( 'NONE', #19638, #2616, #4501 ) ;
#20462=DIRECTION ( 'NONE',  ( -0.8432271980573100567, 0.000000000000000000, 0.5375573387615669718 ) ) ;
#20481=AXIS2_PLACEMENT_3D ( 'NONE', #17376, #12183, #1909 ) ;
#20498=DIRECTION ( 'NONE',  ( 0.000000000000000000, 0.000000000000000000, -1.000000000000000000 ) ) ;
#20500=DIRECTION ( 'NONE',  ( 0.8432271980573223802, 0.000000000000000000, -0.5375573387615476539 ) ) ;
#20523=DIRECTION ( 'NONE',  ( 1.000000000000000000, 0.000000000000000000, 0.000000000000000000 ) ) ;
#20524=CIRCLE ( 'NONE', #13818, 1.100000000000003642 ) ;
#20541=ORIENTED_EDGE ( 'NONE', *, *, #3411, .T. ) ;
#20549=ADVANCED_FACE ( 'NONE', ( #7812 ), #13017, .T. ) ;
#20558=EDGE_CURVE ( 'NONE', #17412, #1609, #9471, .T. ) ;
#20564=AXIS2_PLACEMENT_3D ( 'NONE', #20201, #8378, #13451 ) ;
#20572=CARTESIAN_POINT ( 'NONE',  ( -8.900000000000018119, 0.000000000000000000, -118.9000000000000199 ) ) ;
#20588=CONICAL_SURFACE ( 'NONE', #18467, 103.6249999999999716, 0.5675376247847775391 ) ;
#20594=AXIS2_PLACEMENT_3D ( 'NONE', #8692, #15426, #10453 ) ;
#20601=CARTESIAN_POINT ( 'NONE',  ( -8.000000000000007105, 0.000000000000000000, -104.9000000000000341 ) ) ;
#20640=AXIS2_PLACEMENT_3D ( 'NONE', #10804, #5848, #5734 ) ;
#20647=EDGE_CURVE ( 'NONE', #12372, #5601, #5268, .T. ) ;
#20653=AXIS2_PLACEMENT_3D ( 'NONE', #3453, #11961, #6680 ) ;
#20675=ORIENTED_EDGE ( 'NONE', *, *, #4604, .F. ) ;
#20682=CARTESIAN_POINT ( 'NONE',  ( -10.00000000000002309, 0.000000000000000000, 0.000000000000000000 ) ) ;
#20686=CARTESIAN_POINT ( 'NONE',  ( -7.395800000000001262, 1.287093988729475069E-14, 105.0992000000000104 ) ) ;
#20689=AXIS2_PLACEMENT_3D ( 'NONE', #6091, #20094, #18335 ) ;
#20699=ORIENTED_EDGE ( 'NONE', *, *, #15011, .F. ) ;
#20706=FACE_OUTER_BOUND ( 'NONE', #21024, .T. ) ;
#20723=ORIENTED_EDGE ( 'NONE', *, *, #4323, .F. ) ;
#20725=CARTESIAN_POINT ( 'NONE',  ( -7.440711023145607506, 1.409568465818603827E-14, 115.1000000000000227 ) ) ;
#20730=VERTEX_POINT ( 'NONE', #3924 ) ;
#20744=CARTESIAN_POINT ( 'NONE',  ( 8.000000000000007105, 0.000000000000000000, 0.000000000000000000 ) ) ;
#20751=FACE_OUTER_BOUND ( 'NONE', #14219, .T. ) ;
#20755=CIRCLE ( 'NONE', #18285, 113.8250000000000171 ) ;
#20776=AXIS2_PLACEMENT_3D ( 'NONE', #12099, #18962, #17408 ) ;
#20793=FACE_OUTER_BOUND ( 'NONE', #7097, .T. ) ;
#20795=AXIS2_PLACEMENT_3D ( 'NONE', #12346, #12439, #17428 ) ;
#20797=DIRECTION ( 'NONE',  ( 0.000000000000000000, 0.000000000000000000, -1.000000000000000000 ) ) ;
#20823=CARTESIAN_POINT ( 'NONE',  ( 9.999999999999994671, 0.000000000000000000, 0.000000000000000000 ) ) ;
#20841=ADVANCED_FACE ( 'NONE', ( #18175 ), #8466, .T. ) ;
#20864=CYLINDRICAL_SURFACE ( 'NONE', #10756, 113.8250000000000028 ) ;
#20876=CIRCLE ( 'NONE', #11350, 113.8250000000000028 ) ;
#20882=AXIS2_PLACEMENT_3D ( 'NONE', #13224, #15210, #19975 ) ;
#20883=CIRCLE ( 'NONE', #11358, 115.1000000000000227 ) ;
#20916=CARTESIAN_POINT ( 'NONE',  ( -90.00000000000000000, 0.000000000000000000, -120.0000000000000426 ) ) ;
#20933=AXIS2_PLACEMENT_3D ( 'NONE', #16879, #11795, #8161 ) ;
#20976=DIRECTION ( 'NONE',  ( 1.000000000000000000, 0.000000000000000000, 0.000000000000000000 ) ) ;
#20984=AXIS2_PLACEMENT_3D ( 'NONE', #7324, #8752, #3568 ) ;
#20988=VECTOR ( 'NONE', #20091, 1000.000000000000000 ) ;
#21004=FACE_OUTER_BOUND ( 'NONE', #10932, .T. ) ;
#21014=AXIS2_PLACEMENT_3D ( 'NONE', #6022, #4342, #17720 ) ;
#21024=EDGE_LOOP ( 'NONE', ( #18825, #15581, #20541, #7354 ) ) ;
#21070=ORIENTED_EDGE ( 'NONE', *, *, #19566, .F. ) ;
#21103=EDGE_LOOP ( 'NONE', ( #3090, #10998 ) ) ;
#21130=ORIENTED_EDGE ( 'NONE', *, *, #937, .F. ) ;
#21145=ORIENTED_EDGE ( 'NONE', *, *, #9012, .F. ) ;
#21147=AXIS2_PLACEMENT_3D ( 'NONE', #12445, #14215, #18878 ) ;
#21151=CARTESIAN_POINT ( 'NONE',  ( -10.00000000000002309, 0.000000000000000000, -113.8250000000000028 ) ) ;
#21182=EDGE_CURVE ( 'NONE', #16217, #1841, #10239, .T. ) ;
#21183=FACE_OUTER_BOUND ( 'NONE', #10931, .T. ) ;
#21207=ADVANCED_FACE ( 'NONE', ( #5666 ), #4000, .T. ) ;
#21208=PLANE ( 'NONE',  #19643 ) ;
#21263=AXIS2_PLACEMENT_3D ( 'NONE', #7845, #14583, #1005 ) ;
#21269=CARTESIAN_POINT ( 'NONE',  ( 7.395800000000001262, 0.000000000000000000, 0.000000000000000000 ) ) ;
#21298=CIRCLE ( 'NONE', #11071, 0.2042000000000016025 ) ;
#21330=CARTESIAN_POINT ( 'NONE',  ( -7.600000000000002309, 0.000000000000000000, 0.000000000000000000 ) ) ;
#21343=EDGE_CURVE ( 'NONE', #3351, #2769, #15888, .T. ) ;
#21345=CYLINDRICAL_SURFACE ( 'NONE', #11233, 115.1000000000000227 ) ;
#21362=AXIS2_PLACEMENT_3D ( 'NONE', #14645, #13425, #6594 ) ;
#21375=DIRECTION ( 'NONE',  ( 0.000000000000000000, 0.000000000000000000, -1.000000000000000000 ) ) ;
#21380=ORIENTED_EDGE ( 'NONE', *, *, #3537, .F. ) ;
#21412=ORIENTED_EDGE ( 'NONE', *, *, #13673, .T. ) ;
#21422=DIRECTION ( 'NONE',  ( 0.000000000000000000, 0.000000000000000000, -1.000000000000000000 ) ) ;
#21429=ORIENTED_EDGE ( 'NONE', *, *, #16247, .F. ) ;
#21430=ORIENTED_EDGE ( 'NONE', *, *, #19343, .F. ) ;
#21443=DIRECTION ( 'NONE',  ( 1.000000000000000000, -0.000000000000000000, -0.000000000000000000 ) ) ;
#21513=CARTESIAN_POINT ( 'NONE',  ( 7.440711023145912151, 1.285874240517524538E-14, 104.9000000000000341 ) ) ;
#21529=ORIENTED_EDGE ( 'NONE', *, *, #7315, .T. ) ;
#21573=DIRECTION ( 'NONE',  ( 1.000000000000000000, 0.000000000000000000, 0.000000000000000000 ) ) ;
#21577=STYLED_ITEM ( 'NONE', ( #20267 ), #6478 ) ;
#21609=ORIENTED_EDGE ( 'NONE', *, *, #7315, .F. ) ;
#21636=DIRECTION ( 'NONE',  ( 1.000000000000000000, 0.000000000000000000, 0.000000000000000000 ) ) ;
#21675=FACE_OUTER_BOUND ( 'NONE', #21729, .T. ) ;
#21713=DIRECTION ( 'NONE',  ( 0.000000000000000000, 0.000000000000000000, -1.000000000000000000 ) ) ;
#21717=EDGE_CURVE ( 'NONE', #11505, #8089, #15800, .T. ) ;
#21726=EDGE_LOOP ( 'NONE', ( #14199, #6394 ) ) ;
#21729=EDGE_LOOP ( 'NONE', ( #4394, #19854, #726, #1457 ) ) ;
#21768=AXIS2_PLACEMENT_3D ( 'NONE', #1772, #11823, #15466 ) ;
#21790=FACE_OUTER_BOUND ( 'NONE', #4389, .T. ) ;
#21800=AXIS2_PLACEMENT_3D ( 'NONE', #7473, #735, #6153 ) ;
#21817=VERTEX_POINT ( 'NONE', #10120 ) ;
#21830=STYLED_ITEM ( 'NONE', ( #16999 ), #20339 ) ;
#21833=ORIENTED_EDGE ( 'NONE', *, *, #12983, .F. ) ;
#21834=CARTESIAN_POINT ( 'NONE',  ( -90.00000000000000000, 1.393954219129475159E-14, 113.8250000000000171 ) ) ;
#21837=CARTESIAN_POINT ( 'NONE',  ( 0.000000000000000000, 0.000000000000000000, 0.000000000000000000 ) ) ;
ENDSEC;
END-ISO-10303-21;
